ISO-10303-21;
HEADER;
FILE_DESCRIPTION (('STEP AP214'),
    '1' );
FILE_NAME ('hex flange bolt small_iso_ISO 4162 - M12 x 65 x 65-N.step',
    '2026-10-23T20:35:44',
    ( '' ),
    ( '' ),
    'SwSTEP 2.0',
    'SolidWorks 2025',
    '' );
FILE_SCHEMA (( 'AUTOMOTIVE_DESIGN' ));
ENDSEC;

DATA;
#7=CIRCLE ( 'NONE', #3434, 0.2362204724409449064 ) ;
#14=CIRCLE ( 'NONE', #4286, 0.4629062255509093782 ) ;
#15=( NAMED_UNIT ( * ) PLANE_ANGLE_UNIT ( ) SI_UNIT ( $, .RADIAN. ) );
#17=CARTESIAN_POINT ( 'NONE',  ( 0.4330708661417324024, 0.000000000000000000, 0.000000000000000000 ) ) ;
#34=VERTEX_POINT ( 'NONE', #3752 ) ;
#41=ORIENTED_EDGE ( 'NONE', *, *, #1877, .F. ) ;
#46=CARTESIAN_POINT ( 'NONE',  ( 0.000000000000000000, 2.957312202238506242E-17, 0.2952755905511810774 ) ) ;
#49=EDGE_CURVE ( 'NONE', #4478, #2222, #5824, .T. ) ;
#51=EDGE_CURVE ( 'NONE', #5178, #931, #7181, .T. ) ;
#52=DIRECTION ( 'NONE',  ( -1.000000000000000000, -0.000000000000000000, -0.000000000000000000 ) ) ;
#72=PRODUCT_DEFINITION_SHAPE ( 'NONE', 'NONE',  #5982 ) ;
#77=CARTESIAN_POINT ( 'NONE',  ( 0.3581828924050323715, 0.1743168766271109560, 0.3019256869348722616 ) ) ;
#83=EDGE_CURVE ( 'NONE', #5632, #7112, #5799, .T. ) ;
#87=B_SPLINE_CURVE_WITH_KNOTS ( 'NONE', 3,
 ( #5029, #2125, #4375, #2046, #3150, #6743, #5497, #6139, #1530 ),
 .UNSPECIFIED., .F., .F.,
 ( 4, 2, 1, 2, 4 ),
 ( 0.000000000000000000, 0.002165063509461097064, 0.004330127018922194128, 0.006495190528383291625, 0.008660254037844388256 ),
 .UNSPECIFIED. ) ;
#89=EDGE_LOOP ( 'NONE', ( #2667, #4029, #6739, #4168 ) ) ;
#104=CARTESIAN_POINT ( 'NONE',  ( 0.3411144883932946681, 0.06120045565151401717, -0.3014953316451452481 ) ) ;
#108=AXIS2_PLACEMENT_3D ( 'NONE', #6313, #3367, #512 ) ;
#121=CARTESIAN_POINT ( 'NONE',  ( 0.3410249605999410294, 1.062103031354818709E-12, 0.3014927230551906479 ) ) ;
#136=CARTESIAN_POINT ( 'NONE',  ( 0.3528850351813196395, -0.1886720902358828833, 0.2768301761068310274 ) ) ;
#158=DIRECTION ( 'NONE',  ( 1.000000000000000000, 0.000000000000000000, 0.000000000000000000 ) ) ;
#170=ORIENTED_EDGE ( 'NONE', *, *, #1680, .T. ) ;
#175=CARTESIAN_POINT ( 'NONE',  ( 0.3391216574607823775, -0.1954800165277041091, -0.2519698606119756268 ) ) ;
#178=CARTESIAN_POINT ( 'NONE',  ( 0.3388543739203577765, -0.06138491293039709945, 0.2952755905511811330 ) ) ;
#181=CARTESIAN_POINT ( 'NONE',  ( 0.3581828924050327045, -0.3486337532542230222, -1.123169198254405176E-18 ) ) ;
#187=EDGE_CURVE ( 'NONE', #6581, #698, #1547, .T. ) ;
#198=B_SPLINE_CURVE_WITH_KNOTS ( 'NONE', 3,
 ( #225, #6215, #6608, #5615, #3303, #2545 ),
 .UNSPECIFIED., .F., .F.,
 ( 4, 2, 4 ),
 ( 0.02186578511398849095, 0.02405896738650913774, 0.02625214965902978106 ),
 .UNSPECIFIED. ) ;
#207=CARTESIAN_POINT ( 'NONE',  ( 0.3322361761492156895, 0.2866471735582875047, -0.09406371265339424914 ) ) ;
#219=CARTESIAN_POINT ( 'NONE',  ( 0.4685039370078740717, -0.1704774416898505729, -0.2952755905511810774 ) ) ;
#222=CARTESIAN_POINT ( 'NONE',  ( 0.3485534891173983629, 0.1164145375797932258, -0.3017001449125945034 ) ) ;
#225=CARTESIAN_POINT ( 'NONE',  ( 0.02637295201093697167, 0.1704774416898497680, -0.2952755905511810774 ) ) ;
#228=CARTESIAN_POINT ( 'NONE',  ( 0.3432736861146661878, -0.3267484299055466446, -0.02460629921259840577 ) ) ;
#232=ORIENTED_EDGE ( 'NONE', *, *, #1077, .T. ) ;
#236=ORIENTED_EDGE ( 'NONE', *, *, #249, .T. ) ;
#245=EDGE_CURVE ( 'NONE', #2222, #4734, #1124, .T. ) ;
#249=EDGE_CURVE ( 'NONE', #6858, #951, #2962, .T. ) ;
#254=CARTESIAN_POINT ( 'NONE',  ( 0.3561392902752972267, 0.3446605091515489439, -2.917830865379561131E-17 ) ) ;
#264=CARTESIAN_POINT ( 'NONE',  ( 0.3306743754077735575, 0.2557161625347751932, -0.1476377952755904832 ) ) ;
#265=CARTESIAN_POINT ( 'NONE',  ( 0.3336175750056034062, -0.2273032555864673288, -0.1968503937007873295 ) ) ;
#276=B_SPLINE_CURVE_WITH_KNOTS ( 'NONE', 3,
 ( #1085, #5765, #2842, #7501, #3460, #6940 ),
 .UNSPECIFIED., .F., .F.,
 ( 4, 2, 4 ),
 ( -3.269571951034336179E-06, 0.0001651384380483830793, 0.0003335464480478004612 ),
 .UNSPECIFIED. ) ;
#278=VECTOR ( 'NONE', #577, 39.37007874015748143 ) ;
#295=CARTESIAN_POINT ( 'NONE',  ( 0.000000000000000000, 0.000000000000000000, 0.000000000000000000 ) ) ;
#301=AXIS2_PLACEMENT_3D ( 'NONE', #5704, #2813, #2276 ) ;
#351=CONICAL_SURFACE ( 'NONE', #1424, 0.2952755905511810774, 1.047197551196600518 ) ;
#358=VERTEX_POINT ( 'NONE', #7135 ) ;
#363=ORIENTED_EDGE ( 'NONE', *, *, #1119, .T. ) ;
#364=EDGE_LOOP ( 'NONE', ( #2793, #2733, #2565, #4438 ) ) ;
#366=CARTESIAN_POINT ( 'NONE',  ( 0.3337354549120238878, 0.2853048623713461129, 0.09638866382874489158 ) ) ;
#368=CIRCLE ( 'NONE', #6106, 0.03543307086614165546 ) ;
#376=EDGE_CURVE ( 'NONE', #1383, #931, #426, .T. ) ;
#378=DIRECTION ( 'NONE',  ( 1.000000000000000000, 0.000000000000000000, 0.000000000000000000 ) ) ;
#384=CARTESIAN_POINT ( 'NONE',  ( 0.002513486811083454845, 0.2268523693227592619, 0.1976313516179636909 ) ) ;
#407=CARTESIAN_POINT ( 'NONE',  ( 0.3411151615605803600, 0.2304996462388439749, 0.2037536041052391000 ) ) ;
#412=DIRECTION ( 'NONE',  ( -1.000000000000000000, -0.000000000000000000, -0.000000000000000000 ) ) ;
#418=CARTESIAN_POINT ( 'NONE',  ( 0.000000000000000000, 0.000000000000000000, 0.000000000000000000 ) ) ;
#421=CARTESIAN_POINT ( 'NONE',  ( 0.3479980290963757827, -0.3208941761713900997, 0.04760384692073289098 ) ) ;
#426=CIRCLE ( 'NONE', #548, 0.2952755905511810774 ) ;
#427=EDGE_CURVE ( 'NONE', #4734, #3441, #198, .T. ) ;
#429=DIRECTION ( 'NONE',  ( -1.000000000000000000, -0.000000000000000000, -0.000000000000000000 ) ) ;
#439=AXIS2_PLACEMENT_3D ( 'NONE', #7431, #5193, #1051 ) ;
#446=ORIENTED_EDGE ( 'NONE', *, *, #5897, .F. ) ;
#450=VERTEX_POINT ( 'NONE', #1357 ) ;
#461=CARTESIAN_POINT ( 'NONE',  ( 0.3426144402834003788, -0.2318662757222078041, 0.2014770286013906619 ) ) ;
#472=ORIENTED_EDGE ( 'NONE', *, *, #7389, .F. ) ;
#473=CARTESIAN_POINT ( 'NONE',  ( 0.01168997831664882192, -0.1984671517595423818, -0.2467959906213527677 ) ) ;
#481=EDGE_CURVE ( 'NONE', #2228, #951, #4333, .T. ) ;
#486=EDGE_LOOP ( 'NONE', ( #5349, #1848, #4162 ) ) ;
#496=EDGE_CURVE ( 'NONE', #951, #5211, #3383, .T. ) ;
#501=AXIS2_PLACEMENT_3D ( 'NONE', #5115, #2243, #3385 ) ;
#502=CARTESIAN_POINT ( 'NONE',  ( 0.3485373078438445127, -0.3194486952732369378, -0.05009812457233156491 ) ) ;
#503=FACE_OUTER_BOUND ( 'NONE', #3481, .T. ) ;
#506=LINE ( 'NONE', #4473, #4310 ) ;
#507=( GEOMETRIC_REPRESENTATION_CONTEXT ( 3 ) GLOBAL_UNCERTAINTY_ASSIGNED_CONTEXT ( ( #4584 ) ) GLOBAL_UNIT_ASSIGNED_CONTEXT ( ( #6521, #15, #6473 ) ) REPRESENTATION_CONTEXT ( 'NONE', 'WORKASPACE' ) );
#512=DIRECTION ( 'NONE',  ( 0.000000000000000000, 0.000000000000000000, -1.000000000000000000 ) ) ;
#526=VECTOR ( 'NONE', #2960, 39.37007874015748143 ) ;
#533=ADVANCED_FACE ( 'NONE', ( #4495 ), #6902, .F. ) ;
#537=CARTESIAN_POINT ( 'NONE',  ( 0.3528850351813199726, -0.3340780101605776986, -0.02497973507596915055 ) ) ;
#542=DIRECTION ( 'NONE',  ( 0.000000000000000000, -0.5000000000000005551, 0.8660254037844382635 ) ) ;
#548=AXIS2_PLACEMENT_3D ( 'NONE', #5429, #4233, #3005 ) ;
#553=ORIENTED_EDGE ( 'NONE', *, *, #3600, .F. ) ;
#555=DIRECTION ( 'NONE',  ( 0.000000000000000000, 0.000000000000000000, 1.000000000000000000 ) ) ;
#560=CARTESIAN_POINT ( 'NONE',  ( 0.4685039370078740717, 0.000000000000000000, 0.000000000000000000 ) ) ;
#568=CARTESIAN_POINT ( 'NONE',  ( 0.3306743754077733355, 0.2557161625347751932, 0.1476377952755905942 ) ) ;
#570=CARTESIAN_POINT ( 'NONE',  ( 0.3483227611829846637, -0.1704774416898499345, 0.2952755905511811330 ) ) ;
#577=DIRECTION ( 'NONE',  ( 0.3420201433256623291, 1.150791560227853228E-16, 0.9396926207859106484 ) ) ;
#579=( BOUNDED_SURFACE ( )  B_SPLINE_SURFACE ( 3, 2, ( 
 ( #4765, #2351, #7019 ),
 ( #3619, #1771, #1123 ),
 ( #7095, #1812, #104 ),
 ( #4648, #4110, #4043 ),
 ( #6489, #5338, #6447 ),
 ( #2387, #2882, #4723 ),
 ( #1194, #3539, #1859 ),
 ( #5877, #1702, #639 ) ),
 .UNSPECIFIED., .F., .F., .F. ) 
 B_SPLINE_SURFACE_WITH_KNOTS ( ( 4, 2, 2, 4 ),
 ( 3, 3 ),
 ( 0.03552366018096265315, 0.03995354946645690575, 0.04216849410920403551, 0.04438343875195116528 ),
 ( 0.000000000000000000, 1.000000000000000000 ),
 .UNSPECIFIED. ) 
 GEOMETRIC_REPRESENTATION_ITEM ( )  RATIONAL_B_SPLINE_SURFACE ( (
 ( 1.000000000000000000, 0.8047780977832075244, 1.000000000000000000),
 ( 1.000000000000000000, 0.8123789484488428414, 1.000000000000000000),
 ( 1.000000000000000000, 0.8190677874188468932, 1.000000000000000000),
 ( 1.000000000000000000, 0.8191929099079664489, 1.000000000000000000),
 ( 1.000000000000000000, 0.8176081235728045460, 1.000000000000000000),
 ( 1.000000000000000000, 0.8122952617572927192, 1.000000000000000000),
 ( 1.000000000000000000, 0.8086306736854887989, 1.000000000000000000),
 ( 1.000000000000000000, 0.8047712637616463160, 1.000000000000000000) ) ) 
 REPRESENTATION_ITEM ( '' )  SURFACE ( )  );
#580=EDGE_LOOP ( 'NONE', ( #4258, #6746, #2640, #4665, #5689, #5653, #4951 ) ) ;
#582=B_SPLINE_CURVE_WITH_KNOTS ( 'NONE', 3,
 ( #6808, #3987, #473, #1036, #7411, #1561 ),
 .UNSPECIFIED., .F., .F.,
 ( 4, 2, 4 ),
 ( 2.380732026385019675E-07, 0.002190927868076661400, 0.004381617662950684777 ),
 .UNSPECIFIED. ) ;
#591=( LENGTH_UNIT ( ) NAMED_UNIT ( * ) SI_UNIT ( $, .METRE. ) );
#592=CARTESIAN_POINT ( 'NONE',  ( 0.3585568952266072751, -0.1763490727872195629, 0.3019338363380300039 ) ) ;
#598=CIRCLE ( 'NONE', #108, 0.2952755905511810774 ) ;
#608=ORIENTED_EDGE ( 'NONE', *, *, #83, .T. ) ;
#610=CARTESIAN_POINT ( 'NONE',  ( 0.4685039370078740717, 5.594759879304195485E-17, -0.4507874015748032370 ) ) ;
#613=EDGE_CURVE ( 'NONE', #5211, #5565, #6290, .T. ) ;
#614=VERTEX_POINT ( 'NONE', #46 ) ;
#616=CARTESIAN_POINT ( 'NONE',  ( 0.3997746709170348356, 0.000000000000000000, -0.4629062255509093782 ) ) ;
#620=CARTESIAN_POINT ( 'NONE',  ( 0.3426022948973417304, -0.05819196463765255456, -0.3015401604570891458 ) ) ;
#628=CARTESIAN_POINT ( 'NONE',  ( 0.3479985092864859020, -0.1192235226163089606, 0.3017044423212984494 ) ) ;
#639=CARTESIAN_POINT ( 'NONE',  ( 0.3585664987351884214, -0.1764010263750315499, -0.3019340449705225082 ) ) ;
#663=AXIS2_PLACEMENT_3D ( 'NONE', #6765, #3244, #3283 ) ;
#668=CARTESIAN_POINT ( 'NONE',  ( 0.3465690653189043013, 0.1180910924887165481, 0.2952755905511810774 ) ) ;
#684=CARTESIAN_POINT ( 'NONE',  ( 0.01171324505787554003, 0.3130206113228969356, 0.04838357847483527874 ) ) ;
#694=ADVANCED_FACE ( 'NONE', ( #1693 ), #1141, .T. ) ;
#697=CARTESIAN_POINT ( 'NONE',  ( 0.3410249605999788325, -0.02903799983316278366, -0.3014927230551917026 ) ) ;
#698=VERTEX_POINT ( 'NONE', #5829 ) ;
#704=CARTESIAN_POINT ( 'NONE',  ( 0.3442721343065135997, 0.1485366976410457951, 0.2952755905511810774 ) ) ;
#713=CARTESIAN_POINT ( 'NONE',  ( 0.000000000000000000, 0.000000000000000000, 0.000000000000000000 ) ) ;
#715=B_SPLINE_CURVE_WITH_KNOTS ( 'NONE', 3,
 ( #570, #5234, #1661, #2317, #6988, #4119 ),
 .UNSPECIFIED., .F., .F.,
 ( 4, 2, 4 ),
 ( 0.000000000000000000, 0.0001677595217559109278, 0.0003355190435118218556 ),
 .UNSPECIFIED. ) ;
#726=CARTESIAN_POINT ( 'NONE',  ( 0.4685039370078740717, 0.1704774416898497680, -0.2952755905511810774 ) ) ;
#728=ORIENTED_EDGE ( 'NONE', *, *, #3375, .F. ) ;
#734=LINE ( 'NONE', #3056, #2724 ) ;
#752=ADVANCED_FACE ( 'NONE', ( #814 ), #1606, .F. ) ;
#759=CARTESIAN_POINT ( 'NONE',  ( 0.01834252172841645614, 0.3270457701237517445, 0.02409129084753309363 ) ) ;
#765=CARTESIAN_POINT ( 'NONE',  ( 3.027559055118110187, 2.660472849486257786E-17, -0.1982677165354330695 ) ) ;
#771=CARTESIAN_POINT ( 'NONE',  ( 0.01841426102874288775, 0.1429077274040485568, 0.2952755905511811330 ) ) ;
#773=CARTESIAN_POINT ( 'NONE',  ( 0.3391216574608371670, 0.3159523085418723398, -0.04330572993916122215 ) ) ;
#782=AXIS2_PLACEMENT_3D ( 'NONE', #1020, #6876, #6486 ) ;
#799=CARTESIAN_POINT ( 'NONE',  ( 0.3997746709170348356, 0.000000000000000000, -0.4629062255509093782 ) ) ;
#804=CARTESIAN_POINT ( 'NONE',  ( 0.01832242175888446414, 0.1844213691142423395, 0.2711239997950803393 ) ) ;
#805=CARTESIAN_POINT ( 'NONE',  ( 0.000000000000000000, 0.000000000000000000, 0.000000000000000000 ) ) ;
#808=CARTESIAN_POINT ( 'NONE',  ( 0.002549129251874865387, 0.05807386165059042621, 0.2952755905511811330 ) ) ;
#810=CARTESIAN_POINT ( 'NONE',  ( 0.3409812221349237671, 0.2467127425963012433, -0.1756638922268426994 ) ) ;
#814=FACE_OUTER_BOUND ( 'NONE', #1293, .T. ) ;
#834=CARTESIAN_POINT ( 'NONE',  ( 0.01168997831664888090, -0.3129651733100090039, 0.04847959992982862204 ) ) ;
#840=CARTESIAN_POINT ( 'NONE',  ( 0.3432736861146661322, -0.1846838951640041859, 0.2706692913385828625 ) ) ;
#842=EDGE_CURVE ( 'NONE', #3073, #450, #2024, .T. ) ;
#853=EDGE_LOOP ( 'NONE', ( #3099, #6673, #4483, #2834, #4737 ) ) ;
#859=CARTESIAN_POINT ( 'NONE',  ( 0.3574299024618897702, 0.3465649303883613364, 6.884133197150707104E-16 ) ) ;
#870=CARTESIAN_POINT ( 'NONE',  ( 0.3410425348215777031, 0.2759054741781710729, -0.1251041708914593098 ) ) ;
#881=DIRECTION ( 'NONE',  ( 0.000000000000000000, 0.000000000000000000, -1.000000000000000000 ) ) ;
#890=CARTESIAN_POINT ( 'NONE',  ( 0.02637295201093751290, -0.3409548833797009237, -9.138209691400258722E-18 ) ) ;
#902=ORIENTED_EDGE ( 'NONE', *, *, #6171, .F. ) ;
#905=DIRECTION ( 'NONE',  ( 1.000000000000000000, 0.000000000000000000, -0.000000000000000000 ) ) ;
#913=VERTEX_POINT ( 'NONE', #2606 ) ;
#921=CARTESIAN_POINT ( 'NONE',  ( 0.3565325103478086399, 0.3440765519545058160, 0.005406888575954027845 ) ) ;
#924=ORIENTED_EDGE ( 'NONE', *, *, #2848, .T. ) ;
#931=VERTEX_POINT ( 'NONE', #4484 ) ;
#932=CARTESIAN_POINT ( 'NONE',  ( 0.3391216574609289269, 0.1954800165277119361, 0.2519698606119610829 ) ) ;
#943=EDGE_CURVE ( 'NONE', #4878, #913, #2079, .T. ) ;
#951=VERTEX_POINT ( 'NONE', #1748 ) ;
#957=DIRECTION ( 'NONE',  ( 1.000000000000000000, 0.000000000000000000, 0.000000000000000000 ) ) ;
#974=ORIENTED_EDGE ( 'NONE', *, *, #1349, .T. ) ;
#977=DIRECTION ( 'NONE',  ( 0.000000000000000000, 0.000000000000000000, 1.000000000000000000 ) ) ;
#989=DIRECTION ( 'NONE',  ( -1.000000000000000000, -0.000000000000000000, -0.000000000000000000 ) ) ;
#994=CARTESIAN_POINT ( 'NONE',  ( 0.02637295201093722841, 0.3409548833797004797, 3.882420715168025960E-18 ) ) ;
#999=CARTESIAN_POINT ( 'NONE',  ( 0.4685039370078740717, 0.000000000000000000, 0.2362204724409449064 ) ) ;
#1005=VERTEX_POINT ( 'NONE', #616 ) ;
#1012=DIMENSIONAL_EXPONENTS ( 1.000000000000000000, 0.000000000000000000, 0.000000000000000000, 0.000000000000000000, 0.000000000000000000, 0.000000000000000000, 0.000000000000000000 ) ;
#1020=CARTESIAN_POINT ( 'NONE',  ( 0.4330708661417324024, 5.520553484345353405E-17, -0.4507874015748032370 ) ) ;
#1021=CARTESIAN_POINT ( 'NONE',  ( 0.3321022367507227568, -0.2411754471855062087, 0.1728230530389214537 ) ) ;
#1027=CARTESIAN_POINT ( 'NONE',  ( 0.3336175750056032951, 0.05682581389661665178, 0.2952755905511811885 ) ) ;
#1030=CARTESIAN_POINT ( 'NONE',  ( 0.3997746709170348356, 0.000000000000000000, 0.000000000000000000 ) ) ;
#1035=EDGE_LOOP ( 'NONE', ( #1136, #3060, #3296, #41, #3711 ) ) ;
#1036=CARTESIAN_POINT ( 'NONE',  ( 0.002513486811083733702, -0.2268523693227597338, -0.1976313516179637741 ) ) ;
#1038=ORIENTED_EDGE ( 'NONE', *, *, #6836, .T. ) ;
#1044=CARTESIAN_POINT ( 'NONE',  ( 0.3483227611829846637, 0.1704774416898499345, 0.2952755905511810774 ) ) ;
#1051=DIRECTION ( 'NONE',  ( 0.000000000000000000, 0.000000000000000000, 1.000000000000000000 ) ) ;
#1059=CARTESIAN_POINT ( 'NONE',  ( 0.3391892065151629887, 0.1136516277932332897, 0.2952755905511810774 ) ) ;
#1069=CIRCLE ( 'NONE', #2782, 0.2952755905511810774 ) ;
#1077=EDGE_CURVE ( 'NONE', #2114, #4878, #5583, .T. ) ;
#1085=CARTESIAN_POINT ( 'NONE',  ( 0.3581828924050327045, -0.3486337532542230222, -1.123169198254405176E-18 ) ) ;
#1103=CARTESIAN_POINT ( 'NONE',  ( 0.3527008206095850751, 0.1709223649093223329, 0.2960462201727743214 ) ) ;
#1105=AXIS2_PLACEMENT_3D ( 'NONE', #805, #957, #881 ) ;
#1106=CARTESIAN_POINT ( 'NONE',  ( 0.02637295201093703412, 0.1704774416898499345, 0.2952755905511810774 ) ) ;
#1119=EDGE_CURVE ( 'NONE', #358, #1383, #7289, .T. ) ;
#1123=CARTESIAN_POINT ( 'NONE',  ( 0.3479975484506714345, 0.1192183696110101915, -0.3017044215715822819 ) ) ;
#1124=LINE ( 'NONE', #6236, #3590 ) ;
#1130=CARTESIAN_POINT ( 'NONE',  ( 0.3403864257300880936, 0.2851194846584802489, 0.09670974744601845696 ) ) ;
#1136=ORIENTED_EDGE ( 'NONE', *, *, #4590, .T. ) ;
#1138=CARTESIAN_POINT ( 'NONE',  ( 0.000000000000000000, 0.000000000000000000, 0.000000000000000000 ) ) ;
#1141=CYLINDRICAL_SURFACE ( 'NONE', #2110, 0.2362204724409449064 ) ;
#1153=EDGE_CURVE ( 'NONE', #1896, #3901, #1935, .T. ) ;
#1154=EDGE_CURVE ( 'NONE', #6581, #34, #5730, .T. ) ;
#1158=CARTESIAN_POINT ( 'NONE',  ( 0.3483227611829846637, 0.1704774416898499345, 0.2952755905511810774 ) ) ;
#1174=ORIENTED_EDGE ( 'NONE', *, *, #3375, .T. ) ;
#1185=ORIENTED_EDGE ( 'NONE', *, *, #427, .T. ) ;
#1194=CARTESIAN_POINT ( 'NONE',  ( 0.3442725010713152956, -0.1485386763991280168, -0.2952755905511810774 ) ) ;
#1221=LINE ( 'NONE', #5368, #2900 ) ;
#1244=PLANE ( 'NONE',  #3948 ) ;
#1254=CARTESIAN_POINT ( 'NONE',  ( 0.3528999085283636150, -0.1454870853231272354, -0.3018102362147644380 ) ) ;
#1255=B_SPLINE_CURVE_WITH_KNOTS ( 'NONE', 3,
 ( #2340, #4984, #1490, #4948, #6101, #3797, #7192, #6135 ),
 .UNSPECIFIED., .F., .F.,
 ( 4, 2, 2, 4 ),
 ( 0.004381617662950723809, 0.005472867551409551883, 0.006564117439868379089, 0.008746617216786035237 ),
 .UNSPECIFIED. ) ;
#1279=CARTESIAN_POINT ( 'NONE',  ( 0.3336175750056034617, -0.2841290694830840846, -0.09842519685039370636 ) ) ;
#1280=DIRECTION ( 'NONE',  ( -0.000000000000000000, 0.8660254037844383745, 0.5000000000000006661 ) ) ;
#1289=APPLICATION_CONTEXT ( 'automotive_design' ) ;
#1290=EDGE_CURVE ( 'NONE', #2401, #2222, #3676, .T. ) ;
#1293=EDGE_LOOP ( 'NONE', ( #1989, #3770, #5608, #4332 ) ) ;
#1297=CARTESIAN_POINT ( 'NONE',  ( 0.3585665126877357611, -0.3496831043983833487, 0.001800812819183493984 ) ) ;
#1300=ADVANCED_FACE ( 'NONE', ( #6079 ), #2003, .T. ) ;
#1302=EDGE_CURVE ( 'NONE', #450, #3721, #3853, .T. ) ;
#1310=( LENGTH_UNIT ( ) NAMED_UNIT ( * ) SI_UNIT ( $, .METRE. ) );
#1319=TOROIDAL_SURFACE ( 'NONE', #6834, 0.4507874015748032370, 0.03543307086614166934 ) ;
#1321=CARTESIAN_POINT ( 'NONE',  ( 0.003035684155427131534, 0.2845908893795032757, 0.09762530132584859577 ) ) ;
#1335=EDGE_LOOP ( 'NONE', ( #1893, #4756, #2974, #5553, #2259 ) ) ;
#1338=CARTESIAN_POINT ( 'NONE',  ( 0.3403864257300625029, -0.2851194846584945153, -0.09670974744601064377 ) ) ;
#1349=EDGE_CURVE ( 'NONE', #5600, #1896, #6775, .T. ) ;
#1355=ADVANCED_FACE ( 'NONE', ( #6334 ), #2851, .F. ) ;
#1357=CARTESIAN_POINT ( 'NONE',  ( 0.02637295201093751290, -0.3409548833797009237, -9.138209691400258722E-18 ) ) ;
#1359=AXIS2_PLACEMENT_3D ( 'NONE', #2959, #2852, #5225 ) ;
#1361=CARTESIAN_POINT ( 'NONE',  ( 0.3425764178929367465, 0.2322094954269895706, -0.2008802154383052541 ) ) ;
#1374=PLANE ( 'NONE',  #7171 ) ;
#1376=CARTESIAN_POINT ( 'NONE',  ( 0.3321022367507226458, 0.2411754471855206694, -0.1728230530388957520 ) ) ;
#1383=VERTEX_POINT ( 'NONE', #4076 ) ;
#1387=CONICAL_SURFACE ( 'NONE', #439, 0.1982677165354330695, 0.7853981633974452814 ) ;
#1390=CARTESIAN_POINT ( 'NONE',  ( 0.004822332172886080806, 0.2197023059474403073, -0.2100156246613533173 ) ) ;
#1399=FACE_OUTER_BOUND ( 'NONE', #7029, .T. ) ;
#1406=DIRECTION ( 'NONE',  ( -1.000000000000000000, 0.000000000000000000, -0.000000000000000000 ) ) ;
#1408=CARTESIAN_POINT ( 'NONE',  ( 0.3403864257301138507, 0.2263128404110440195, -0.1985658431051529893 ) ) ;
#1412=AXIS2_PLACEMENT_3D ( 'NONE', #4879, #2131, #4422 ) ;
#1415=ORIENTED_EDGE ( 'NONE', *, *, #3600, .T. ) ;
#1424=AXIS2_PLACEMENT_3D ( 'NONE', #4083, #5203, #5846 ) ;
#1428=CARTESIAN_POINT ( 'NONE',  ( 0.3391892065151630442, 0.3125419764313920878, -0.04921259842519681155 ) ) ;
#1447=ORIENTED_EDGE ( 'NONE', *, *, #4387, .T. ) ;
#1465=DIRECTION ( 'NONE',  ( 0.000000000000000000, 0.000000000000000000, 1.000000000000000000 ) ) ;
#1471=EDGE_CURVE ( 'NONE', #4570, #5600, #4405, .T. ) ;
#1472=AXIS2_PLACEMENT_3D ( 'NONE', #2508, #7205, #3813 ) ;
#1486=EDGE_CURVE ( 'NONE', #5632, #1005, #4075, .T. ) ;
#1490=CARTESIAN_POINT ( 'NONE',  ( 0.0006233585804809438748, -0.2412158484082067011, 0.1727530760685163091 ) ) ;
#1502=CARTESIAN_POINT ( 'NONE',  ( 0.0006233585804807679088, 0.2412158484082065346, -0.1727530760685158651 ) ) ;
#1503=AXIS2_PLACEMENT_3D ( 'NONE', #3855, #378, #6113 ) ;
#1515=CARTESIAN_POINT ( 'NONE',  ( 0.01836325778988931109, -0.1427310470019619582, -0.2952755905511810774 ) ) ;
#1530=CARTESIAN_POINT ( 'NONE',  ( 0.3483227611829848303, -0.1704774416898505729, -0.2952755905511810774 ) ) ;
#1532=CARTESIAN_POINT ( 'NONE',  ( 0.3409812221349194372, 0.2754857644942527717, 0.1258275564122752488 ) ) ;
#1547=B_SPLINE_CURVE_WITH_KNOTS ( 'NONE', 3,
 ( #1704, #2313, #2279, #5810, #2256, #1027, #1059, #4513, #6377 ),
 .UNSPECIFIED., .F., .F.,
 ( 4, 2, 1, 2, 4 ),
 ( 0.000000000000000000, 0.002165063509461094028, 0.004330127018922188056, 0.006495190528383282084, 0.008660254037844376113 ),
 .UNSPECIFIED. ) ;
#1552=SHAPE_REPRESENTATION ( 'hex flange bolt small_iso_ISO 4162 - M12 x 65 x 65-N', ( #5166 ), #1726 ) ;
#1561=CARTESIAN_POINT ( 'NONE',  ( 0.000000000000000000, -0.2557161625347750822, -0.1476377952755907330 ) ) ;
#1575=CARTESIAN_POINT ( 'NONE',  ( 0.3531511627980717938, 0.3349346966101464096, 0.02350890366534340997 ) ) ;
#1587=ADVANCED_FACE ( 'NONE', ( #3461 ), #1387, .T. ) ;
#1591=CARTESIAN_POINT ( 'NONE',  ( 0.3528971332113847725, -0.1886393090946611450, -0.2768874834731246404 ) ) ;
#1592=CARTESIAN_POINT ( 'NONE',  ( 0.3411151615605706455, -0.2917056203871725706, 0.09774174715353350917 ) ) ;
#1606=( BOUNDED_SURFACE ( )  B_SPLINE_SURFACE ( 3, 2, ( 
 ( #2453, #6024, #3104 ),
 ( #175, #5322, #2533 ),
 ( #1888, #3726, #3024 ),
 ( #3144, #4335, #3642 ),
 ( #6557, #1338, #3061 ),
 ( #2498, #5907, #6064 ),
 ( #6668, #4830, #4178 ),
 ( #7156, #7189, #1297 ) ),
 .UNSPECIFIED., .F., .F., .F. ) 
 B_SPLINE_SURFACE_WITH_KNOTS ( ( 4, 2, 2, 4 ),
 ( 3, 3 ),
 ( 0.03551798592901340978, 0.03994769179990649566, 0.04216254473535303859, 0.04437739767079958153 ),
 ( 0.000000000000000000, 1.000000000000000000 ),
 .UNSPECIFIED. ) 
 GEOMETRIC_REPRESENTATION_ITEM ( )  RATIONAL_B_SPLINE_SURFACE ( (
 ( 1.000000000000000000, 0.8047781103519396906, 1.000000000000000000),
 ( 1.000000000000000000, 0.8123785826170297764, 1.000000000000000000),
 ( 1.000000000000000000, 0.8190671539034730664, 1.000000000000000000),
 ( 1.000000000000000000, 0.8191932076449999212, 1.000000000000000000),
 ( 1.000000000000000000, 0.8176085094066802839, 1.000000000000000000),
 ( 1.000000000000000000, 0.8122955484013585359, 1.000000000000000000),
 ( 1.000000000000000000, 0.8086308001281159452, 1.000000000000000000),
 ( 1.000000000000000000, 0.8047712537969721192, 1.000000000000000000) ) ) 
 REPRESENTATION_ITEM ( '' )  SURFACE ( )  );
#1613=ORIENTED_EDGE ( 'NONE', *, *, #3137, .F. ) ;
#1615=ORIENTED_EDGE ( 'NONE', *, *, #842, .T. ) ;
#1619=ORIENTED_EDGE ( 'NONE', *, *, #613, .T. ) ;
#1635=CARTESIAN_POINT ( 'NONE',  ( -2.349015779708382802E-16, 0.2702383257424525453, -0.1224846707640857985 ) ) ;
#1639=EDGE_CURVE ( 'NONE', #7488, #6858, #2662, .T. ) ;
#1646=ORIENTED_EDGE ( 'NONE', *, *, #3657, .F. ) ;
#1649=CARTESIAN_POINT ( 'NONE',  ( 0.3581828924050324825, 0.3486337532542225226, 1.056976728655274672E-17 ) ) ;
#1661=CARTESIAN_POINT ( 'NONE',  ( 0.3527008206095850196, -0.1709223649093223885, 0.2960462201727743770 ) ) ;
#1666=FACE_OUTER_BOUND ( 'NONE', #580, .T. ) ;
#1680=EDGE_CURVE ( 'NONE', #2401, #358, #1221, .T. ) ;
#1693=FACE_OUTER_BOUND ( 'NONE', #89, .T. ) ;
#1696=CIRCLE ( 'NONE', #4748, 0.2952755905511810774 ) ;
#1702=CARTESIAN_POINT ( 'NONE',  ( 0.3565422129079688918, -0.1767726971815447856, -0.2952755905511810774 ) ) ;
#1704=CARTESIAN_POINT ( 'NONE',  ( 0.3483227611829846637, -0.1704774416898499345, 0.2952755905511811330 ) ) ;
#1714=ADVANCED_FACE ( 'NONE', ( #5416 ), #3714, .F. ) ;
#1715=FACE_OUTER_BOUND ( 'NONE', #7164, .T. ) ;
#1726=( GEOMETRIC_REPRESENTATION_CONTEXT ( 3 ) GLOBAL_UNCERTAINTY_ASSIGNED_CONTEXT ( ( #3116 ) ) GLOBAL_UNIT_ASSIGNED_CONTEXT ( ( #4344, #1897, #5502 ) ) REPRESENTATION_CONTEXT ( 'NONE', 'WORKASPACE' ) );
#1727=CARTESIAN_POINT ( 'NONE',  ( 0.4685039370078740717, -0.3409548833797009237, 0.000000000000000000 ) ) ;
#1733=DIRECTION ( 'NONE',  ( -0.000000000000000000, 0.000000000000000000, -1.000000000000000000 ) ) ;
#1741=FACE_OUTER_BOUND ( 'NONE', #5613, .T. ) ;
#1748=CARTESIAN_POINT ( 'NONE',  ( 2.989606299212598017, 2.892866454678787531E-17, -0.2362204724409449064 ) ) ;
#1770=DIRECTION ( 'NONE',  ( 1.000000000000000000, 0.000000000000000000, 0.000000000000000000 ) ) ;
#1771=CARTESIAN_POINT ( 'NONE',  ( 0.3459458835994366765, 0.1200656956960832605, -0.2952755905511810774 ) ) ;
#1781=CARTESIAN_POINT ( 'NONE',  ( 2.989606299212598017, 0.000000000000000000, 0.000000000000000000 ) ) ;
#1800=CARTESIAN_POINT ( 'NONE',  ( 2.989606299212598017, 0.000000000000000000, 0.2362204724409449064 ) ) ;
#1802=PLANE ( 'NONE',  #6018 ) ;
#1812=CARTESIAN_POINT ( 'NONE',  ( 0.3388530074223801147, 0.06137376066181338130, -0.2952755905511810774 ) ) ;
#1821=CARTESIAN_POINT ( 'NONE',  ( 0.4330708661417324024, 0.000000000000000000, 0.4507874015748032370 ) ) ;
#1845=CARTESIAN_POINT ( 'NONE',  ( 0.3510870379221574522, 0.1475852640829200257, 0.2952755905511810774 ) ) ;
#1848=ORIENTED_EDGE ( 'NONE', *, *, #2275, .T. ) ;
#1850=CARTESIAN_POINT ( 'NONE',  ( 0.3485777078273626928, -0.3195689143662223120, 0.04989192643193118837 ) ) ;
#1859=CARTESIAN_POINT ( 'NONE',  ( 0.3531513458567848707, -0.1471090214728858203, -0.3018164116569697075 ) ) ;
#1877=EDGE_CURVE ( 'NONE', #698, #2114, #3402, .T. ) ;
#1884=DIRECTION ( 'NONE',  ( 1.000000000000000000, 0.000000000000000000, -0.000000000000000000 ) ) ;
#1888=CARTESIAN_POINT ( 'NONE',  ( 0.3322361761492684806, -0.2247851515112275766, -0.2012118778978489453 ) ) ;
#1893=ORIENTED_EDGE ( 'NONE', *, *, #1680, .F. ) ;
#1896=VERTEX_POINT ( 'NONE', #7492 ) ;
#1897=( NAMED_UNIT ( * ) PLANE_ANGLE_UNIT ( ) SI_UNIT ( $, .RADIAN. ) );
#1900=( BOUNDED_SURFACE ( )  B_SPLINE_SURFACE ( 3, 2, ( 
 ( #4507, #2704, #7438 ),
 ( #2211, #7401, #421 ),
 ( #3974, #2173, #1592 ),
 ( #1021, #6266, #6303 ),
 ( #3240, #6840, #461 ),
 ( #3856, #2780, #4470 ),
 ( #6228, #5588, #3391 ),
 ( #5048, #5124, #4543 ) ),
 .UNSPECIFIED., .F., .F., .F. ) 
 B_SPLINE_SURFACE_WITH_KNOTS ( ( 4, 2, 2, 4 ),
 ( 3, 3 ),
 ( 0.03551798592901338203, 0.03994769179990646790, 0.04216254473535301084, 0.04437739767079956071 ),
 ( 0.000000000000000000, 1.000000000000000000 ),
 .UNSPECIFIED. ) 
 GEOMETRIC_REPRESENTATION_ITEM ( )  RATIONAL_B_SPLINE_SURFACE ( (
 ( 1.000000000000000000, 0.8047781103519389134, 1.000000000000000000),
 ( 1.000000000000000000, 0.8123785826170312196, 1.000000000000000000),
 ( 1.000000000000000000, 0.8190671539034724002, 1.000000000000000000),
 ( 1.000000000000000000, 0.8191932076449992550, 1.000000000000000000),
 ( 1.000000000000000000, 0.8176085094069774906, 1.000000000000000000),
 ( 1.000000000000000000, 0.8122955484010631055, 1.000000000000000000),
 ( 1.000000000000000000, 0.8086308001283356583, 1.000000000000000000),
 ( 1.000000000000000000, 0.8047712537969732294, 1.000000000000000000) ) ) 
 REPRESENTATION_ITEM ( '' )  SURFACE ( )  );
#1904=CARTESIAN_POINT ( 'NONE',  ( 0.3432736861146659657, 0.1846838951640041582, 0.2706692913385826960 ) ) ;
#1912=CARTESIAN_POINT ( 'NONE',  ( 0.3483227611829849413, -0.3409548833797009237, 0.000000000000000000 ) ) ;
#1917=EDGE_LOOP ( 'NONE', ( #4560, #3806, #2596, #5450, #2322 ) ) ;
#1929=CARTESIAN_POINT ( 'NONE',  ( 0.3403859949404050012, 0.05880135802647309951, 0.2952755905511811330 ) ) ;
#1932=CARTESIAN_POINT ( 'NONE',  ( 0.3565325103478085289, 0.1673557731150444039, 0.3006824791271354158 ) ) ;
#1935=LINE ( 'NONE', #219, #6015 ) ;
#1942=CARTESIAN_POINT ( 'NONE',  ( 0.3485373078438441796, 0.2031105961982143382, -0.2516016230262507203 ) ) ;
#1955=DIRECTION ( 'NONE',  ( 1.000000000000000000, 0.000000000000000000, -0.000000000000000000 ) ) ;
#1957=CARTESIAN_POINT ( 'NONE',  ( 0.3496779274129792059, 0.3447056852546006578, 0.006496579416451838881 ) ) ;
#1962=ADVANCED_FACE ( 'NONE', ( #1399 ), #4870, .T. ) ;
#1975=EDGE_CURVE ( 'NONE', #6027, #1005, #3710, .T. ) ;
#1977=DIRECTION ( 'NONE',  ( 0.000000000000000000, 0.000000000000000000, -1.000000000000000000 ) ) ;
#1989=ORIENTED_EDGE ( 'NONE', *, *, #3880, .T. ) ;
#2003=CONICAL_SURFACE ( 'NONE', #1503, 0.2952755905511810774, 1.047197551196600518 ) ;
#2019=CARTESIAN_POINT ( 'NONE',  ( 0.3426147637089220765, 0.05832033309504411345, -0.3015404986019938893 ) ) ;
#2024=B_SPLINE_CURVE_WITH_KNOTS ( 'NONE', 3,
 ( #7341, #6778, #5098, #3218, #2120, #3838, #6132, #890 ),
 .UNSPECIFIED., .F., .F.,
 ( 4, 2, 2, 4 ),
 ( 0.004381617662950684777, 0.005472867551409519790, 0.006564117439868355670, 0.008746617216786024829 ),
 .UNSPECIFIED. ) ;
#2030=B_SPLINE_CURVE_WITH_KNOTS ( 'NONE', 3,
 ( #1912, #2554, #7216, #3824, #4892, #4850, #3094, #840, #2594 ),
 .UNSPECIFIED., .F., .F.,
 ( 4, 2, 1, 2, 4 ),
 ( 0.000000000000000000, 0.002165063509461098799, 0.004330127018922199332, 0.006495190528383298564, 0.008660254037844398664 ),
 .UNSPECIFIED. ) ;
#2033=CARTESIAN_POINT ( 'NONE',  ( 0.01165389088406399223, -0.1143408654217484000, -0.2952755905511810219 ) ) ;
#2042=CARTESIAN_POINT ( 'NONE',  ( 0.3432736861146661322, 0.3267484299055463115, 0.02460629921259843353 ) ) ;
#2046=CARTESIAN_POINT ( 'NONE',  ( 0.3336175750056032396, 0.05682581389661631177, -0.2952755905511810219 ) ) ;
#2061=CARTESIAN_POINT ( 'NONE',  ( 0.3561390657006783811, -0.1723301304999994843, -0.2984845417009731050 ) ) ;
#2079=LINE ( 'NONE', #6419, #278 ) ;
#2091=CARTESIAN_POINT ( 'NONE',  ( 0.000000000000000000, 0.2557161625347749712, -0.1476377952755909551 ) ) ;
#2096=CARTESIAN_POINT ( 'NONE',  ( 0.3336175750056032396, 0.2841290694830835850, -0.09842519685039363697 ) ) ;
#2108=CARTESIAN_POINT ( 'NONE',  ( 0.01168997831664858947, 0.1984671517595417711, 0.2467959906213527677 ) ) ;
#2110=AXIS2_PLACEMENT_3D ( 'NONE', #4031, #5796, #555 ) ;
#2114=VERTEX_POINT ( 'NONE', #3706 ) ;
#2120=CARTESIAN_POINT ( 'NONE',  ( 0.004822332172886453772, -0.2917300191221102734, -0.08525996588982823199 ) ) ;
#2125=CARTESIAN_POINT ( 'NONE',  ( 0.3432736861146659657, 0.1420645347415414039, -0.2952755905511810219 ) ) ;
#2127=ORIENTED_EDGE ( 'NONE', *, *, #2978, .F. ) ;
#2131=DIRECTION ( 'NONE',  ( 1.000000000000000000, 0.000000000000000000, 0.000000000000000000 ) ) ;
#2134=DIRECTION ( 'NONE',  ( 0.000000000000000000, 0.000000000000000000, 1.000000000000000000 ) ) ;
#2151=CARTESIAN_POINT ( 'NONE',  ( 0.3410425348215775920, 0.2462961272004790259, 0.1763890642357578975 ) ) ;
#2160=CARTESIAN_POINT ( 'NONE',  ( 0.3487102105009254327, 0.3201373431253348167, 0.04891434758976444946 ) ) ;
#2162=CARTESIAN_POINT ( 'NONE',  ( 0.000000000000000000, 0.000000000000000000, -0.2952755905511810774 ) ) ;
#2173=CARTESIAN_POINT ( 'NONE',  ( 0.3388536909602617997, -0.2864058322153867353, 0.09448172812127884901 ) ) ;
#2190=CARTESIAN_POINT ( 'NONE',  ( 0.3425764178929368575, 0.2900721174007582781, 0.1006592143205869566 ) ) ;
#2196=CARTESIAN_POINT ( 'NONE',  ( 0.3388536909603142577, 0.2250264928541962084, 0.2007938624298919450 ) ) ;
#2201=DIRECTION ( 'NONE',  ( -1.000000000000000000, -0.000000000000000000, -0.000000000000000000 ) ) ;
#2204=TOROIDAL_SURFACE ( 'NONE', #501, 0.4507874015748032370, 0.03543307086614166934 ) ;
#2211=CARTESIAN_POINT ( 'NONE',  ( 0.3391216574608478806, -0.3159523085418498023, 0.04330572993920116937 ) ) ;
#2222=VERTEX_POINT ( 'NONE', #6523 ) ;
#2226=CIRCLE ( 'NONE', #5407, 0.2362204724409449064 ) ;
#2228=VERTEX_POINT ( 'NONE', #1800 ) ;
#2243=DIRECTION ( 'NONE',  ( -1.000000000000000000, -0.000000000000000000, -0.000000000000000000 ) ) ;
#2248=CARTESIAN_POINT ( 'NONE',  ( 0.3581828924050324825, 0.3486337532542225226, 1.056976728655274672E-17 ) ) ;
#2255=EDGE_CURVE ( 'NONE', #3901, #3073, #582, .T. ) ;
#2256=CARTESIAN_POINT ( 'NONE',  ( 0.3306743754077733910, -1.707404996040164512E-17, 0.2952755905511811885 ) ) ;
#2259=ORIENTED_EDGE ( 'NONE', *, *, #1119, .F. ) ;
#2268=CARTESIAN_POINT ( 'NONE',  ( 0.3410249605999032263, -0.02920150297965336608, 0.3014927230551895931 ) ) ;
#2273=PRODUCT_DEFINITION_FORMATION_WITH_SPECIFIED_SOURCE ( 'ANY', '', #6010, .NOT_KNOWN. ) ;
#2275=EDGE_CURVE ( 'NONE', #614, #3721, #598, .T. ) ;
#2276=DIRECTION ( 'NONE',  ( 1.000000000000000000, 0.000000000000000000, 0.000000000000000000 ) ) ;
#2277=DIRECTION ( 'NONE',  ( 0.000000000000000000, 0.000000000000000000, -1.000000000000000000 ) ) ;
#2279=CARTESIAN_POINT ( 'NONE',  ( 0.3391892065151629332, -0.1136516277932332758, 0.2952755905511811885 ) ) ;
#2303=DIRECTION ( 'NONE',  ( 0.000000000000000000, 0.5000000000000018874, 0.8660254037844375974 ) ) ;
#2308=CIRCLE ( 'NONE', #6234, 0.4629062255509093782 ) ;
#2313=CARTESIAN_POINT ( 'NONE',  ( 0.3432736861146659657, -0.1420645347415416260, 0.2952755905511810774 ) ) ;
#2314=CARTESIAN_POINT ( 'NONE',  ( 0.3483227611829848303, 0.3409548833797004797, 0.000000000000000000 ) ) ;
#2317=CARTESIAN_POINT ( 'NONE',  ( 0.3561392902752972267, -0.1723302545757742776, 0.2984847566065203517 ) ) ;
#2322=ORIENTED_EDGE ( 'NONE', *, *, #3893, .F. ) ;
#2326=CARTESIAN_POINT ( 'NONE',  ( 3.027559055118110187, 0.000000000000000000, 0.000000000000000000 ) ) ;
#2331=ADVANCED_FACE ( 'NONE', ( #3356 ), #1900, .F. ) ;
#2335=( BOUNDED_SURFACE ( )  B_SPLINE_SURFACE ( 3, 2, ( 
 ( #1957, #921, #4445 ),
 ( #773, #3100, #5448 ),
 ( #207, #6628, #2528 ),
 ( #1376, #3722, #810 ),
 ( #3140, #1408, #4899 ),
 ( #4331, #3757, #3178 ),
 ( #6849, #3951, #4594 ),
 ( #6809, #7373, #5137 ) ),
 .UNSPECIFIED., .F., .F., .F. ) 
 B_SPLINE_SURFACE_WITH_KNOTS ( ( 4, 2, 2, 4 ),
 ( 3, 3 ),
 ( 0.03551798592901333346, 0.03994769179990642627, 0.04216254473535296921, 0.04437739767079951908 ),
 ( 0.000000000000000000, 1.000000000000000000 ),
 .UNSPECIFIED. ) 
 GEOMETRIC_REPRESENTATION_ITEM ( )  RATIONAL_B_SPLINE_SURFACE ( (
 ( 1.000000000000000000, 0.8047781103519390244, 1.000000000000000000),
 ( 1.000000000000000000, 0.8123785826175446978, 1.000000000000000000),
 ( 1.000000000000000000, 0.8190671539027887249, 1.000000000000000000),
 ( 1.000000000000000000, 0.8191932076453414258, 1.000000000000000000),
 ( 1.000000000000000000, 0.8176085094066379844, 1.000000000000000000),
 ( 1.000000000000000000, 0.8122955484014008354, 1.000000000000000000),
 ( 1.000000000000000000, 0.8086308001280824165, 1.000000000000000000),
 ( 1.000000000000000000, 0.8047712537969731184, 1.000000000000000000) ) ) 
 REPRESENTATION_ITEM ( '' )  SURFACE ( )  );
#2340=CARTESIAN_POINT ( 'NONE',  ( 0.000000000000000000, -0.2557161625347748601, 0.1476377952755911216 ) ) ;
#2341=CARTESIAN_POINT ( 'NONE',  ( 0.3391221370943153790, -0.1204748818123362597, 0.2952755905511811330 ) ) ;
#2351=CARTESIAN_POINT ( 'NONE',  ( 0.3565325281581928074, 0.1767208741530144900, -0.2952755905511811330 ) ) ;
#2368=PLANE ( 'NONE',  #3082 ) ;
#2373=ADVANCED_FACE ( 'NONE', ( #503 ), #1319, .T. ) ;
#2387=CARTESIAN_POINT ( 'NONE',  ( 0.3398315730591770500, -0.1188962366173021562, -0.2952755905511810774 ) ) ;
#2401=VERTEX_POINT ( 'NONE', #5347 ) ;
#2403=CARTESIAN_POINT ( 'NONE',  ( 0.3426022948973417859, 0.05819196463765207578, 0.3015401604570892014 ) ) ;
#2416=LENGTH_MEASURE_WITH_UNIT ( LENGTH_MEASURE( 0.02539999999999999897 ), #591 );
#2422=DIRECTION ( 'NONE',  ( 1.000000000000000000, 0.000000000000000000, -0.000000000000000000 ) ) ;
#2424=ORIENTED_EDGE ( 'NONE', *, *, #3034, .T. ) ;
#2430=ADVANCED_FACE ( 'NONE', ( #6539 ), #5852, .T. ) ;
#2432=CONICAL_SURFACE ( 'NONE', #1412, 0.2952755905511810774, 1.047197551196600518 ) ;
#2453=CARTESIAN_POINT ( 'NONE',  ( 0.3496779274129793169, -0.1667266398149501727, -0.3017721699676331748 ) ) ;
#2457=CARTESIAN_POINT ( 'NONE',  ( 0.02637295201093723881, -0.1704774416898505729, -0.2952755905511810774 ) ) ;
#2461=VERTEX_POINT ( 'NONE', #6048 ) ;
#2484=CARTESIAN_POINT ( 'NONE',  ( 0.3997746709170348356, 0.000000000000000000, 0.000000000000000000 ) ) ;
#2493=CARTESIAN_POINT ( 'NONE',  ( 0.000000000000000000, 2.957312202238506242E-17, 0.2952755905511810774 ) ) ;
#2498=CARTESIAN_POINT ( 'NONE',  ( 0.3398312250858251948, -0.3151631602416472555, -0.04467257488985885983 ) ) ;
#2500=DIRECTION ( 'NONE',  ( -1.000000000000000000, -0.000000000000000000, -0.000000000000000000 ) ) ;
#2503=DIRECTION ( 'NONE',  ( -1.000000000000000000, -0.000000000000000000, -0.000000000000000000 ) ) ;
#2508=CARTESIAN_POINT ( 'NONE',  ( 0.000000000000000000, 0.000000000000000000, 0.000000000000000000 ) ) ;
#2512=CARTESIAN_POINT ( 'NONE',  ( 0.3581828924050323715, 0.1743168766271107895, -0.3019256869348722061 ) ) ;
#2528=CARTESIAN_POINT ( 'NONE',  ( 0.3411151615605715337, 0.2917056203871458142, -0.09774174715358552312 ) ) ;
#2529=FACE_OUTER_BOUND ( 'NONE', #3183, .T. ) ;
#2533=CARTESIAN_POINT ( 'NONE',  ( 0.3479980290963871625, -0.2016732288369692816, -0.2541005850305417257 ) ) ;
#2538=B_SPLINE_CURVE_WITH_KNOTS ( 'NONE', 3,
 ( #2493, #6060, #808, #3176, #771, #3138 ),
 .UNSPECIFIED., .F., .F.,
 ( 4, 2, 4 ),
 ( 0.01227927579290655560, 0.01447189347357576844, 0.01666451115424498128 ),
 .UNSPECIFIED. ) ;
#2545=CARTESIAN_POINT ( 'NONE',  ( 0.000000000000000000, 0.000000000000000000, -0.2952755905511810774 ) ) ;
#2546=DIRECTION ( 'NONE',  ( -1.000000000000000000, -0.000000000000000000, 0.000000000000000000 ) ) ;
#2554=CARTESIAN_POINT ( 'NONE',  ( 0.3432736861146661878, -0.3267484299055466446, 0.02460629921259842312 ) ) ;
#2559=CARTESIAN_POINT ( 'NONE',  ( 0.3485616995351332181, 0.1165012447190262312, 0.3017003685801735724 ) ) ;
#2565=ORIENTED_EDGE ( 'NONE', *, *, #3880, .F. ) ;
#2582=CARTESIAN_POINT ( 'NONE',  ( 0.01171324505787542034, 0.1984117137466533121, -0.2468920120763460069 ) ) ;
#2589=CARTESIAN_POINT ( 'NONE',  ( 0.0006233585804808155053, 0.2702164766613434077, 0.1225225144826656842 ) ) ;
#2594=CARTESIAN_POINT ( 'NONE',  ( 0.3483227611829846637, -0.1704774416898499345, 0.2952755905511811330 ) ) ;
#2596=ORIENTED_EDGE ( 'NONE', *, *, #5431, .T. ) ;
#2597=CARTESIAN_POINT ( 'NONE',  ( 0.3505601438611538057, 0.1704774416898496292, -0.2952755905511812995 ) ) ;
#2606=CARTESIAN_POINT ( 'NONE',  ( 0.3997746709170348356, 5.668966274263039413E-17, 0.4629062255509093782 ) ) ;
#2614=DIRECTION ( 'NONE',  ( 0.000000000000000000, 0.000000000000000000, 1.000000000000000000 ) ) ;
#2636=CARTESIAN_POINT ( 'NONE',  ( 0.000000000000000000, 0.000000000000000000, 0.000000000000000000 ) ) ;
#2640=ORIENTED_EDGE ( 'NONE', *, *, #6603, .T. ) ;
#2652=CARTESIAN_POINT ( 'NONE',  ( 3.027559055118110187, 0.000000000000000000, 0.000000000000000000 ) ) ;
#2660=CARTESIAN_POINT ( 'NONE',  ( 0.3483227611829846082, 0.1704774416898497680, -0.2952755905511810774 ) ) ;
#2662=CIRCLE ( 'NONE', #6216, 0.1982677165354330695 ) ;
#2667=ORIENTED_EDGE ( 'NONE', *, *, #481, .T. ) ;
#2679=ORIENTED_EDGE ( 'NONE', *, *, #49, .F. ) ;
#2687=EDGE_LOOP ( 'NONE', ( #4252, #5217, #170, #5144, #5057 ) ) ;
#2702=CARTESIAN_POINT ( 'NONE',  ( 0.02637295201093751290, -0.3409548833797009237, -9.138209691400258722E-18 ) ) ;
#2704=CARTESIAN_POINT ( 'NONE',  ( 0.3565325103478088065, -0.3440765519545064266, -0.005406888575953978406 ) ) ;
#2724=VECTOR ( 'NONE', #2901, 39.37007874015748143 ) ;
#2729=CARTESIAN_POINT ( 'NONE',  ( 0.3581828924050323715, 0.1743168766271109560, 0.3019256869348722616 ) ) ;
#2733=ORIENTED_EDGE ( 'NONE', *, *, #5801, .F. ) ;
#2741=DIRECTION ( 'NONE',  ( 1.000000000000000000, 0.000000000000000000, 0.000000000000000000 ) ) ;
#2754=EDGE_CURVE ( 'NONE', #3441, #1383, #1696, .T. ) ;
#2755=ORIENTED_EDGE ( 'NONE', *, *, #5938, .F. ) ;
#2766=CARTESIAN_POINT ( 'NONE',  ( 0.3565422270302657237, 0.3441025489056184772, -0.005451916616122978385 ) ) ;
#2771=ORIENTED_EDGE ( 'NONE', *, *, #376, .F. ) ;
#2780=CARTESIAN_POINT ( 'NONE',  ( 0.3465694189147059956, -0.1966695024996656382, 0.2499096104736426016 ) ) ;
#2782=AXIS2_PLACEMENT_3D ( 'NONE', #2636, #1955, #6122 ) ;
#2793=ORIENTED_EDGE ( 'NONE', *, *, #4590, .F. ) ;
#2796=CARTESIAN_POINT ( 'NONE',  ( 0.3410076799406683290, 0.2754140928391118348, 0.1259532371559686781 ) ) ;
#2813=DIRECTION ( 'NONE',  ( -0.000000000000000000, 0.000000000000000000, 1.000000000000000000 ) ) ;
#2821=CARTESIAN_POINT ( 'NONE',  ( 0.3581828924050323715, 0.1743168766271107895, -0.3019256869348722061 ) ) ;
#2832=CONICAL_SURFACE ( 'NONE', #7115, 0.4629062255509093782, 1.221730476396037490 ) ;
#2834=ORIENTED_EDGE ( 'NONE', *, *, #7091, .F. ) ;
#2842=CARTESIAN_POINT ( 'NONE',  ( 0.3561390657006787142, -0.3446602609999988021, 5.012419073868498717E-17 ) ) ;
#2848=EDGE_CURVE ( 'NONE', #3022, #2114, #4504, .T. ) ;
#2851=PLANE ( 'NONE',  #301 ) ;
#2852=DIRECTION ( 'NONE',  ( 0.000000000000000000, -0.8660254037844381525, -0.5000000000000009992 ) ) ;
#2859=CARTESIAN_POINT ( 'NONE',  ( 0.4685039370078740717, -0.1704774416898505729, -0.2952755905511810774 ) ) ;
#2872=DIRECTION ( 'NONE',  ( 0.000000000000000000, 0.000000000000000000, -1.000000000000000000 ) ) ;
#2882=CARTESIAN_POINT ( 'NONE',  ( 0.3465697713329959906, -0.1180955399632931530, -0.2952755905511810774 ) ) ;
#2884=CARTESIAN_POINT ( 'NONE',  ( 0.3336175750056032396, 0.2841290694830835850, 0.09842519685039366473 ) ) ;
#2900=VECTOR ( 'NONE', #52, 39.37007874015748143 ) ;
#2901=DIRECTION ( 'NONE',  ( -1.000000000000000000, -0.000000000000000000, -0.000000000000000000 ) ) ;
#2902=CARTESIAN_POINT ( 'NONE',  ( 0.3485777078273625817, 0.3195689143662219234, -0.04989192643193119531 ) ) ;
#2909=CARTESIAN_POINT ( 'NONE',  ( 0.3411158341578399145, -0.06121148758009550134, 0.3014953708557878698 ) ) ;
#2915=CIRCLE ( 'NONE', #3663, 0.1982677165354330695 ) ;
#2959=CARTESIAN_POINT ( 'NONE',  ( 0.4685039370078740717, 0.3409548833797004797, 0.000000000000000000 ) ) ;
#2960=DIRECTION ( 'NONE',  ( -1.000000000000000000, -0.000000000000000000, -0.000000000000000000 ) ) ;
#2962=LINE ( 'NONE', #3504, #6052 ) ;
#2970=ORIENTED_EDGE ( 'NONE', *, *, #4351, .F. ) ;
#2974=ORIENTED_EDGE ( 'NONE', *, *, #245, .T. ) ;
#2976=AXIS2_PLACEMENT_3D ( 'NONE', #6328, #5152, #2872 ) ;
#2978=EDGE_CURVE ( 'NONE', #7112, #5632, #6711, .T. ) ;
#2980=ORIENTED_EDGE ( 'NONE', *, *, #613, .F. ) ;
#2999=DIRECTION ( 'NONE',  ( -1.000000000000000000, -0.000000000000000000, -0.000000000000000000 ) ) ;
#3005=DIRECTION ( 'NONE',  ( 0.000000000000000000, 0.000000000000000000, -1.000000000000000000 ) ) ;
#3009=DIRECTION ( 'NONE',  ( 0.000000000000000000, 0.000000000000000000, -1.000000000000000000 ) ) ;
#3015=ORIENTED_EDGE ( 'NONE', *, *, #1302, .T. ) ;
#3020=FACE_OUTER_BOUND ( 'NONE', #1917, .T. ) ;
#3022=VERTEX_POINT ( 'NONE', #2248 ) ;
#3024=CARTESIAN_POINT ( 'NONE',  ( 0.3411151615605753085, -0.2304996462388200218, -0.2037536041052529223 ) ) ;
#3028=CARTESIAN_POINT ( 'NONE',  ( 0.01836325778988323956, -0.1427310470019406141, 0.2952755905511810774 ) ) ;
#3034=EDGE_CURVE ( 'NONE', #1896, #7420, #5319, .T. ) ;
#3041=PRODUCT_DEFINITION_CONTEXT ( 'detailed design', #1289, 'design' ) ;
#3056=CARTESIAN_POINT ( 'NONE',  ( 0.4685039370078740717, 0.1704774416898499345, 0.2952755905511810774 ) ) ;
#3057=CIRCLE ( 'NONE', #7206, 0.2952755905511810774 ) ;
#3060=ORIENTED_EDGE ( 'NONE', *, *, #3262, .F. ) ;
#3061=CARTESIAN_POINT ( 'NONE',  ( 0.3426144402833997127, -0.2904173629089126796, -0.1000635707556142007 ) ) ;
#3065=CARTESIAN_POINT ( 'NONE',  ( 0.02637295201093707228, -0.1704774416898499345, 0.2952755905511811330 ) ) ;
#3066=CARTESIAN_POINT ( 'NONE',  ( 0.3565324925542818213, -0.1767206836160838956, 0.2952755905511811885 ) ) ;
#3071=CARTESIAN_POINT ( 'NONE',  ( 0.3410425348215776475, -0.2759054741781712949, 0.1251041708914593653 ) ) ;
#3073=VERTEX_POINT ( 'NONE', #6045 ) ;
#3082=AXIS2_PLACEMENT_3D ( 'NONE', #4701, #6465, #5360 ) ;
#3087=DIRECTION ( 'NONE',  ( 0.000000000000000000, -1.000000000000000000, 0.000000000000000000 ) ) ;
#3092=EDGE_CURVE ( 'NONE', #931, #358, #5966, .T. ) ;
#3094=CARTESIAN_POINT ( 'NONE',  ( 0.3391892065151629332, -0.1988903486381584651, 0.2460629921259843145 ) ) ;
#3096=ORIENTED_EDGE ( 'NONE', *, *, #3938, .F. ) ;
#3099=ORIENTED_EDGE ( 'NONE', *, *, #245, .F. ) ;
#3100=CARTESIAN_POINT ( 'NONE',  ( 0.3459463601587655091, 0.3157502742998894996, -0.04365566351111115767 ) ) ;
#3104=CARTESIAN_POINT ( 'NONE',  ( 0.3585569128062319755, -0.1733077889112134284, -0.3036897776982950825 ) ) ;
#3115=CARTESIAN_POINT ( 'NONE',  ( 0.3410249605999031153, 0.02920150297965299485, -0.3014927230551893711 ) ) ;
#3116=UNCERTAINTY_MEASURE_WITH_UNIT (LENGTH_MEASURE( 1.000000000000000082E-05 ), #4344, 'distance_accuracy_value', 'NONE');
#3118=EDGE_CURVE ( 'NONE', #7112, #913, #368, .T. ) ;
#3123=DIRECTION ( 'NONE',  ( 0.000000000000000000, 0.000000000000000000, -1.000000000000000000 ) ) ;
#3131=CARTESIAN_POINT ( 'NONE',  ( 0.3561390657006783811, 0.1723301304999986516, -0.2984845417009731605 ) ) ;
#3137=EDGE_CURVE ( 'NONE', #4478, #3022, #3491, .T. ) ;
#3138=CARTESIAN_POINT ( 'NONE',  ( 0.02637295201093703412, 0.1704774416898499345, 0.2952755905511810774 ) ) ;
#3140=CARTESIAN_POINT ( 'NONE',  ( 0.3337354549120237213, 0.2261274626982069103, -0.1988869267224314119 ) ) ;
#3142=AXIS2_PLACEMENT_3D ( 'NONE', #2326, #4663, #4283 ) ;
#3144=CARTESIAN_POINT ( 'NONE',  ( 0.3321022367506965556, -0.2702568778840481745, -0.1224525375122541698 ) ) ;
#3150=CARTESIAN_POINT ( 'NONE',  ( 0.3306743754077733910, -4.012401740694386787E-16, -0.2952755905511810774 ) ) ;
#3155=LENGTH_MEASURE_WITH_UNIT ( LENGTH_MEASURE( 0.02539999999999999897 ), #1310 );
#3163=CARTESIAN_POINT ( 'NONE',  ( 0.000000000000000000, -0.2557161625347748601, 0.1476377952755911216 ) ) ;
#3176=CARTESIAN_POINT ( 'NONE',  ( 0.01178921041716320811, 0.1149842948508782436, 0.2952755905511810774 ) ) ;
#3177=ORIENTED_EDGE ( 'NONE', *, *, #7514, .T. ) ;
#3178=CARTESIAN_POINT ( 'NONE',  ( 0.3487102105009307618, 0.2024297391849447236, -0.2527898980517343519 ) ) ;
#3183=EDGE_LOOP ( 'NONE', ( #2127, #7269 ) ) ;
#3194=B_SPLINE_CURVE_WITH_KNOTS ( 'NONE', 3,
 ( #5859, #1254, #4666, #620, #697, #5279 ),
 .UNSPECIFIED., .F., .F.,
 ( 4, 2, 4 ),
 ( 0.000000000000000000, 0.002233368740102889029, 0.004466737480205778058 ),
 .UNSPECIFIED. ) ;
#3211=CARTESIAN_POINT ( 'NONE',  ( 0.01832242175888456129, 0.3270109559553079359, -0.02415159075610075201 ) ) ;
#3218=CARTESIAN_POINT ( 'NONE',  ( 0.003035684155427393477, -0.2845908893795038308, -0.09762530132584867903 ) ) ;
#3235=DIRECTION ( 'NONE',  ( -1.000000000000000000, -0.000000000000000000, -0.000000000000000000 ) ) ;
#3237=CARTESIAN_POINT ( 'NONE',  ( 0.3483227611829849413, -0.3409548833797009237, 0.000000000000000000 ) ) ;
#3240=CARTESIAN_POINT ( 'NONE',  ( 0.3337354549120238878, -0.2261274626982048841, 0.1988869267224354920 ) ) ;
#3244=DIRECTION ( 'NONE',  ( -1.000000000000000000, -0.000000000000000000, -0.000000000000000000 ) ) ;
#3255=APPLICATION_CONTEXT ( 'automotive_design' ) ;
#3261=CARTESIAN_POINT ( 'NONE',  ( 0.3426144402834028768, 0.2904173629089201736, 0.1000635707556194326 ) ) ;
#3262=EDGE_CURVE ( 'NONE', #4878, #2461, #4038, .T. ) ;
#3281=EDGE_LOOP ( 'NONE', ( #446, #3628, #7452, #3096, #6663 ) ) ;
#3283=DIRECTION ( 'NONE',  ( 0.000000000000000000, 0.000000000000000000, 1.000000000000000000 ) ) ;
#3296=ORIENTED_EDGE ( 'NONE', *, *, #1077, .F. ) ;
#3303=CARTESIAN_POINT ( 'NONE',  ( -2.614463900186501485E-17, 0.02884736746568806673, -0.2952755905511810774 ) ) ;
#3318=CARTESIAN_POINT ( 'NONE',  ( 0.3410249605999410294, 1.062103031354818709E-12, 0.3014927230551906479 ) ) ;
#3356=FACE_OUTER_BOUND ( 'NONE', #364, .T. ) ;
#3367=DIRECTION ( 'NONE',  ( 1.000000000000000000, 0.000000000000000000, -0.000000000000000000 ) ) ;
#3375=EDGE_CURVE ( 'NONE', #6858, #7488, #2915, .T. ) ;
#3383=LINE ( 'NONE', #7392, #6656 ) ;
#3385=DIRECTION ( 'NONE',  ( 0.000000000000000000, 0.000000000000000000, 1.000000000000000000 ) ) ;
#3391=CARTESIAN_POINT ( 'NONE',  ( 0.3531511627980793433, -0.1878266560944103492, 0.2783075040405565415 ) ) ;
#3399=CARTESIAN_POINT ( 'NONE',  ( 0.000000000000000000, 0.2557161625347749712, -0.1476377952755909551 ) ) ;
#3402=B_SPLINE_CURVE_WITH_KNOTS ( 'NONE', 3,
 ( #1044, #3960, #1103, #3919, #5145, #2729 ),
 .UNSPECIFIED., .F., .F.,
 ( 4, 2, 4 ),
 ( 0.000000000000000000, 0.0001677595217559110904, 0.0003355190435118221809 ),
 .UNSPECIFIED. ) ;
#3410=ORIENTED_EDGE ( 'NONE', *, *, #3137, .T. ) ;
#3422=CARTESIAN_POINT ( 'NONE',  ( 0.4685039370078740717, 0.3409548833797004797, 2.164902785881980513E-17 ) ) ;
#3434=AXIS2_PLACEMENT_3D ( 'NONE', #1781, #4122, #3673 ) ;
#3437=DIRECTION ( 'NONE',  ( -1.000000000000000000, -0.000000000000000000, -0.000000000000000000 ) ) ;
#3441=VERTEX_POINT ( 'NONE', #2162 ) ;
#3457=ORIENTED_EDGE ( 'NONE', *, *, #6645, .T. ) ;
#3460=CARTESIAN_POINT ( 'NONE',  ( 0.3505601438611543053, -0.3409548833797009237, 1.488710258487716964E-17 ) ) ;
#3461=FACE_OUTER_BOUND ( 'NONE', #6741, .T. ) ;
#3465=ADVANCED_FACE ( 'NONE', ( #7092 ), #4720, .T. ) ;
#3468=CARTESIAN_POINT ( 'NONE',  ( 0.3485777078273626373, -0.2029921329169081246, -0.2518088348849962799 ) ) ;
#3470=FACE_OUTER_BOUND ( 'NONE', #5419, .T. ) ;
#3474=CARTESIAN_POINT ( 'NONE',  ( 0.3336175750056032396, 0.2273032555864667459, 0.1968503937007873295 ) ) ;
#3481=EDGE_LOOP ( 'NONE', ( #5651, #5417, #1646, #6734 ) ) ;
#3486=CARTESIAN_POINT ( 'NONE',  ( 0.3485534891173986405, -0.1164145375797935450, 0.3017001449125945034 ) ) ;
#3491=B_SPLINE_CURVE_WITH_KNOTS ( 'NONE', 3,
 ( #2512, #7172, #1942, #1361, #3707, #870, #5948, #2902, #5903, #6935 ),
 .UNSPECIFIED., .F., .F.,
 ( 4, 2, 2, 2, 4 ),
 ( 0.000000000000000000, 0.002239656411828510989, 0.004479312823657021977, 0.006718969235485534701, 0.008958625647314047424 ),
 .UNSPECIFIED. ) ;
#3492=CARTESIAN_POINT ( 'NONE',  ( 0.01165389088405563781, -0.1143408654217081682, 0.2952755905511811885 ) ) ;
#3504=CARTESIAN_POINT ( 'NONE',  ( 3.027559055118110187, 2.428079244293728657E-17, -0.1982677165354330695 ) ) ;
#3509=ADVANCED_FACE ( 'NONE', ( #5187, #2529 ), #4569, .T. ) ;
#3519=VECTOR ( 'NONE', #4890, 39.37007874015748143 ) ;
#3531=ORIENTED_EDGE ( 'NONE', *, *, #1486, .F. ) ;
#3539=CARTESIAN_POINT ( 'NONE',  ( 0.3510874053966554498, -0.1475872118127406207, -0.2952755905511810774 ) ) ;
#3546=CARTESIAN_POINT ( 'NONE',  ( 0.3581828924050327045, -0.3486337532542230222, -1.123169198254405176E-18 ) ) ;
#3552=CONICAL_SURFACE ( 'NONE', #1105, 0.2952755905511810774, 1.047197551196600518 ) ;
#3568=CARTESIAN_POINT ( 'NONE',  ( 0.3398308759505395682, 0.1188917464549260616, 0.2952755905511810774 ) ) ;
#3590=VECTOR ( 'NONE', #429, 39.37007874015748143 ) ;
#3592=ADVANCED_FACE ( 'NONE', ( #7246 ), #2432, .T. ) ;
#3600=EDGE_CURVE ( 'NONE', #3721, #3073, #6111, .T. ) ;
#3607=CARTESIAN_POINT ( 'NONE',  ( 0.3387173876318818611, 0.02883917696872971906, 0.2952755905511811330 ) ) ;
#3619=CARTESIAN_POINT ( 'NONE',  ( 0.3391211773724056577, 0.1204696997606904962, -0.2952755905511810774 ) ) ;
#3627=CARTESIAN_POINT ( 'NONE',  ( 0.000000000000000000, 0.000000000000000000, 0.000000000000000000 ) ) ;
#3628=ORIENTED_EDGE ( 'NONE', *, *, #5801, .T. ) ;
#3635=DIRECTION ( 'NONE',  ( -1.000000000000000000, -0.000000000000000000, -0.000000000000000000 ) ) ;
#3642=CARTESIAN_POINT ( 'NONE',  ( 0.3409812221349221573, -0.2754857644942658168, -0.1258275564122679768 ) ) ;
#3644=EDGE_CURVE ( 'NONE', #1383, #4734, #3675, .T. ) ;
#3654=ORIENTED_EDGE ( 'NONE', *, *, #6171, .T. ) ;
#3657=EDGE_CURVE ( 'NONE', #913, #1005, #2308, .T. ) ;
#3663=AXIS2_PLACEMENT_3D ( 'NONE', #2652, #412, #5077 ) ;
#3673=DIRECTION ( 'NONE',  ( 0.000000000000000000, 0.000000000000000000, 1.000000000000000000 ) ) ;
#3675=B_SPLINE_CURVE_WITH_KNOTS ( 'NONE', 3,
 ( #2091, #3773, #1502, #5581, #1390, #2582, #4920, #4345 ),
 .UNSPECIFIED., .F., .F.,
 ( 4, 2, 2, 4 ),
 ( 0.004381617662950710798, 0.005472867551409541474, 0.006564117439868372150, 0.008746617216786031768 ),
 .UNSPECIFIED. ) ;
#3676=B_SPLINE_CURVE_WITH_KNOTS ( 'NONE', 3,
 ( #6155, #5665, #1428, #2096, #264, #4966, #6759, #3779, #2660 ),
 .UNSPECIFIED., .F., .F.,
 ( 4, 2, 1, 2, 4 ),
 ( 2.312923578716022130E-20, 0.002165063509461098365, 0.004330127018922196730, 0.006495190528383295095, 0.008660254037844393460 ),
 .UNSPECIFIED. ) ;
#3680=EDGE_LOOP ( 'NONE', ( #7311, #728 ) ) ;
#3683=ORIENTED_EDGE ( 'NONE', *, *, #2255, .F. ) ;
#3690=CARTESIAN_POINT ( 'NONE',  ( 3.027559055118110187, 0.000000000000000000, 0.000000000000000000 ) ) ;
#3706=CARTESIAN_POINT ( 'NONE',  ( 0.3581828924050323715, 0.1743168766271109560, 0.3019256869348722616 ) ) ;
#3707=CARTESIAN_POINT ( 'NONE',  ( 0.3410076799406683845, 0.2467857494855107137, -0.1755389823809322958 ) ) ;
#3710=LINE ( 'NONE', #799, #3519 ) ;
#3711=ORIENTED_EDGE ( 'NONE', *, *, #187, .F. ) ;
#3714=( BOUNDED_SURFACE ( )  B_SPLINE_SURFACE ( 3, 2, ( 
 ( #5867, #3066, #592 ),
 ( #2341, #4752, #628 ),
 ( #4832, #178, #2909 ),
 ( #7159, #3607, #4138 ),
 ( #6475, #1929, #7125 ),
 ( #3568, #668, #7084 ),
 ( #704, #1845, #6522 ),
 ( #5255, #4260, #6596 ) ),
 .UNSPECIFIED., .F., .F., .F. ) 
 B_SPLINE_SURFACE_WITH_KNOTS ( ( 4, 2, 2, 4 ),
 ( 3, 3 ),
 ( 0.03551233549299846748, 0.03994185813602711688, 0.04215661945754144158, 0.04437138077905577321 ),
 ( 0.000000000000000000, 1.000000000000000000 ),
 .UNSPECIFIED. ) 
 GEOMETRIC_REPRESENTATION_ITEM ( )  RATIONAL_B_SPLINE_SURFACE ( (
 ( 1.000000000000000000, 0.8047781229087798138, 1.000000000000000000),
 ( 1.000000000000000000, 0.8123782171506571670, 1.000000000000000000),
 ( 1.000000000000000000, 0.8190665209243362943, 1.000000000000000000),
 ( 1.000000000000000000, 0.8191935049886309717, 1.000000000000000000),
 ( 1.000000000000000000, 0.8176088963536531917, 1.000000000000000000),
 ( 1.000000000000000000, 0.8122958360081882212, 1.000000000000000000),
 ( 1.000000000000000000, 0.8086309270602213273, 1.000000000000000000),
 ( 1.000000000000000000, 0.8047712437947333042, 1.000000000000000000) ) ) 
 REPRESENTATION_ITEM ( '' )  SURFACE ( )  );
#3720=CARTESIAN_POINT ( 'NONE',  ( 3.027559055118110187, 0.000000000000000000, 0.000000000000000000 ) ) ;
#3721=VERTEX_POINT ( 'NONE', #7314 ) ;
#3722=CARTESIAN_POINT ( 'NONE',  ( 0.3387177083556421331, 0.2412911239081777792, -0.1726226950780199998 ) ) ;
#3726=CARTESIAN_POINT ( 'NONE',  ( 0.3388536909603144798, -0.2250264928541644005, -0.2007938624299156205 ) ) ;
#3733=EDGE_LOOP ( 'NONE', ( #4521, #4088, #5358, #472 ) ) ;
#3740=ADVANCED_FACE ( 'NONE', ( #7467 ), #2204, .T. ) ;
#3752=CARTESIAN_POINT ( 'NONE',  ( 0.02637295201093707228, -0.1704774416898499345, 0.2952755905511811330 ) ) ;
#3753=CARTESIAN_POINT ( 'NONE',  ( 0.4685039370078740717, 0.000000000000000000, 0.4507874015748032370 ) ) ;
#3757=CARTESIAN_POINT ( 'NONE',  ( 0.3465694189146783510, 0.1966695024996976682, -0.2499096104736449331 ) ) ;
#3759=ORIENTED_EDGE ( 'NONE', *, *, #5150, .F. ) ;
#3767=CARTESIAN_POINT ( 'NONE',  ( 0.3483227611829848303, 0.3409548833797004797, 0.000000000000000000 ) ) ;
#3769=CARTESIAN_POINT ( 'NONE',  ( 0.3485373078438442351, -0.2031105961982146157, 0.2516016230262508313 ) ) ;
#3770=ORIENTED_EDGE ( 'NONE', *, *, #3034, .F. ) ;
#3773=CARTESIAN_POINT ( 'NONE',  ( -2.403706095987794643E-16, 0.2484822268960368286, -0.1601673393405684265 ) ) ;
#3779=CARTESIAN_POINT ( 'NONE',  ( 0.3432736861146659102, 0.1846838951640040472, -0.2706692913385826404 ) ) ;
#3797=CARTESIAN_POINT ( 'NONE',  ( 0.01171324505787554697, -0.1984117137466534231, 0.2468920120763462012 ) ) ;
#3806=ORIENTED_EDGE ( 'NONE', *, *, #187, .T. ) ;
#3813=DIRECTION ( 'NONE',  ( 0.000000000000000000, 0.000000000000000000, -1.000000000000000000 ) ) ;
#3816=CARTESIAN_POINT ( 'NONE',  ( 3.027559055118110187, 0.000000000000000000, 0.1982677165354330695 ) ) ;
#3824=CARTESIAN_POINT ( 'NONE',  ( 0.3336175750056034617, -0.2841290694830839736, 0.09842519685039370636 ) ) ;
#3828=CARTESIAN_POINT ( 'NONE',  ( 0.002479217192763490639, -0.05744896992510376693, -0.2952755905511810774 ) ) ;
#3838=CARTESIAN_POINT ( 'NONE',  ( 0.01171324505787584534, -0.3130206113228972131, -0.04838357847483532731 ) ) ;
#3853=B_SPLINE_CURVE_WITH_KNOTS ( 'NONE', 3,
 ( #2702, #5550, #834, #7400, #5047, #3163 ),
 .UNSPECIFIED., .F., .F.,
 ( 4, 2, 4 ),
 ( 2.380732026380333730E-07, 0.002190927868076681349, 0.004381617662950723809 ),
 .UNSPECIFIED. ) ;
#3855=CARTESIAN_POINT ( 'NONE',  ( 0.000000000000000000, 0.000000000000000000, 0.000000000000000000 ) ) ;
#3856=CARTESIAN_POINT ( 'NONE',  ( 0.3398312250857989381, -0.1962691648279019652, 0.2506030156613254789 ) ) ;
#3877=CARTESIAN_POINT ( 'NONE',  ( 0.3387177083556158763, 0.2701412011613934516, 0.1226528954731279514 ) ) ;
#3880=EDGE_CURVE ( 'NONE', #4570, #7420, #276, .T. ) ;
#3893=EDGE_CURVE ( 'NONE', #34, #614, #5482, .T. ) ;
#3896=AXIS2_PLACEMENT_3D ( 'NONE', #3627, #5472, #4321 ) ;
#3901=VERTEX_POINT ( 'NONE', #2457 ) ;
#3913=MANIFOLD_SOLID_BREP ( 'FlangeHexFillet', #3968 ) ;
#3919=CARTESIAN_POINT ( 'NONE',  ( 0.3561392902752972267, 0.1723302545757742221, 0.2984847566065203517 ) ) ;
#3923=CARTESIAN_POINT ( 'NONE',  ( 0.3479980290963966549, 0.2016732288369792181, 0.2541005850305664282 ) ) ;
#3924=ORIENTED_EDGE ( 'NONE', *, *, #5161, .T. ) ;
#3938=EDGE_CURVE ( 'NONE', #3721, #34, #1255, .T. ) ;
#3948=AXIS2_PLACEMENT_3D ( 'NONE', #726, #5888, #6384 ) ;
#3949=DIMENSIONAL_EXPONENTS ( 1.000000000000000000, 0.000000000000000000, 0.000000000000000000, 0.000000000000000000, 0.000000000000000000, 0.000000000000000000, 0.000000000000000000 ) ;
#3951=CARTESIAN_POINT ( 'NONE',  ( 0.3510872220067887683, 0.1819230426404221390, -0.2754512281816320352 ) ) ;
#3956=CARTESIAN_POINT ( 'NONE',  ( 0.3581828924050323715, 0.1743168766271109560, 0.3019256869348722616 ) ) ;
#3960=CARTESIAN_POINT ( 'NONE',  ( 0.3505602286436571013, 0.1704774416898499345, 0.2952755905511810774 ) ) ;
#3968=CLOSED_SHELL ( 'NONE', ( #2373, #2430, #4307, #694, #3509, #3465, #1587, #4353, #4962, #3740, #6454, #7134, #1300, #3592, #1962, #6179, #4595, #1355, #4635, #533, #5440, #4955, #5724, #2331, #752, #1714, #6092, #6646, #5564 ) ) ;
#3974=CARTESIAN_POINT ( 'NONE',  ( 0.3322361761492158561, -0.2866471735583170366, 0.09406371265334383114 ) ) ;
#3987=CARTESIAN_POINT ( 'NONE',  ( 0.01832242175888466190, -0.1844213691142429778, -0.2711239997950803393 ) ) ;
#4014=ORIENTED_EDGE ( 'NONE', *, *, #496, .F. ) ;
#4025=CARTESIAN_POINT ( 'NONE',  ( 0.4685039370078740717, 2.892866454678787531E-17, -0.2362204724409449064 ) ) ;
#4029=ORIENTED_EDGE ( 'NONE', *, *, #496, .T. ) ;
#4031=CARTESIAN_POINT ( 'NONE',  ( 0.000000000000000000, 0.000000000000000000, 0.000000000000000000 ) ) ;
#4038=B_SPLINE_CURVE_WITH_KNOTS ( 'NONE', 3,
 ( #7495, #2268, #5792, #3486, #5249, #5695 ),
 .UNSPECIFIED., .F., .F.,
 ( 4, 2, 4 ),
 ( 0.004466737480205772853, 0.006712681563759903200, 0.008958625647314033547 ),
 .UNSPECIFIED. ) ;
#4040=CARTESIAN_POINT ( 'NONE',  ( 0.3410076799406688286, -0.2754140928391124454, -0.1259532371559686781 ) ) ;
#4043=CARTESIAN_POINT ( 'NONE',  ( 0.3409815385080205985, -0.02878389060673587282, -0.3014914578570770387 ) ) ;
#4060=ORIENTED_EDGE ( 'NONE', *, *, #481, .F. ) ;
#4065=DIRECTION ( 'NONE',  ( 0.000000000000000000, 0.8660254037844375974, -0.5000000000000018874 ) ) ;
#4075=CIRCLE ( 'NONE', #782, 0.03543307086614165546 ) ;
#4076=CARTESIAN_POINT ( 'NONE',  ( 0.000000000000000000, 0.2557161625347749712, -0.1476377952755909551 ) ) ;
#4077=CARTESIAN_POINT ( 'NONE',  ( 0.3997746709170348356, 0.000000000000000000, 0.000000000000000000 ) ) ;
#4083=CARTESIAN_POINT ( 'NONE',  ( 0.000000000000000000, 0.000000000000000000, 0.000000000000000000 ) ) ;
#4088=ORIENTED_EDGE ( 'NONE', *, *, #2848, .F. ) ;
#4100=DIRECTION ( 'NONE',  ( 0.000000000000000000, 0.000000000000000000, 1.000000000000000000 ) ) ;
#4110=CARTESIAN_POINT ( 'NONE',  ( 0.3387180295041032907, -0.02886098700874997411, -0.2952755905511810219 ) ) ;
#4119=CARTESIAN_POINT ( 'NONE',  ( 0.3581828924050323715, -0.1743168766271109560, 0.3019256869348722616 ) ) ;
#4122=DIRECTION ( 'NONE',  ( -1.000000000000000000, -0.000000000000000000, -0.000000000000000000 ) ) ;
#4126=CARTESIAN_POINT ( 'NONE',  ( 0.3528999085283635040, 0.1454870853231265693, 0.3018102362147644380 ) ) ;
#4138=CARTESIAN_POINT ( 'NONE',  ( 0.3409809061799574659, 0.02876216262209277050, 0.3014914394333951253 ) ) ;
#4150=CARTESIAN_POINT ( 'NONE',  ( 0.000000000000000000, 0.000000000000000000, 0.2362204724409449064 ) ) ;
#4162=ORIENTED_EDGE ( 'NONE', *, *, #3938, .T. ) ;
#4168=ORIENTED_EDGE ( 'NONE', *, *, #6125, .F. ) ;
#4178=CARTESIAN_POINT ( 'NONE',  ( 0.3531511627980769008, -0.3349346966101605649, -0.02350890366535178522 ) ) ;
#4181=CARTESIAN_POINT ( 'NONE',  ( 0.000000000000000000, 2.957312202238506242E-17, 0.2952755905511810774 ) ) ;
#4200=FACE_OUTER_BOUND ( 'NONE', #4620, .T. ) ;
#4233=DIRECTION ( 'NONE',  ( 1.000000000000000000, 0.000000000000000000, -0.000000000000000000 ) ) ;
#4234=CARTESIAN_POINT ( 'NONE',  ( 0.3391892065151629332, 0.1988903486381583818, 0.2460629921259842312 ) ) ;
#4252=ORIENTED_EDGE ( 'NONE', *, *, #5431, .F. ) ;
#4258=ORIENTED_EDGE ( 'NONE', *, *, #943, .F. ) ;
#4260=CARTESIAN_POINT ( 'NONE',  ( 0.3565422412058069090, 0.1767728485866832400, 0.2952755905511811330 ) ) ;
#4283=DIRECTION ( 'NONE',  ( 0.000000000000000000, 0.000000000000000000, 1.000000000000000000 ) ) ;
#4285=FACE_OUTER_BOUND ( 'NONE', #4912, .T. ) ;
#4286=AXIS2_PLACEMENT_3D ( 'NONE', #1030, #3437, #5778 ) ;
#4307=ADVANCED_FACE ( 'NONE', ( #1715 ), #6435, .T. ) ;
#4310=VECTOR ( 'NONE', #989, 39.37007874015748143 ) ;
#4318=CARTESIAN_POINT ( 'NONE',  ( 0.3391892065151631552, -0.1988903486381589925, -0.2460629921259842035 ) ) ;
#4321=DIRECTION ( 'NONE',  ( 0.000000000000000000, 0.000000000000000000, -1.000000000000000000 ) ) ;
#4331=CARTESIAN_POINT ( 'NONE',  ( 0.3398312250857988270, 0.1962691648278992451, -0.2506030156613296422 ) ) ;
#4332=ORIENTED_EDGE ( 'NONE', *, *, #1471, .F. ) ;
#4333=CIRCLE ( 'NONE', #5303, 0.2362204724409449064 ) ;
#4335=CARTESIAN_POINT ( 'NONE',  ( 0.3387177083556159873, -0.2701412011614057196, -0.1226528954731239129 ) ) ;
#4344=( CONVERSION_BASED_UNIT ( 'INCH', #3155 ) LENGTH_UNIT ( ) NAMED_UNIT ( #3949 ) );
#4345=CARTESIAN_POINT ( 'NONE',  ( 0.02637295201093697167, 0.1704774416898497680, -0.2952755905511810774 ) ) ;
#4350=CARTESIAN_POINT ( 'NONE',  ( 0.3581828924050324825, -0.1743168766271116221, -0.3019256869348722061 ) ) ;
#4351=EDGE_CURVE ( 'NONE', #3073, #3441, #1069, .T. ) ;
#4353=ADVANCED_FACE ( 'NONE', ( #6017 ), #1374, .F. ) ;
#4361=CARTESIAN_POINT ( 'NONE',  ( 0.02637295201093723881, -0.1704774416898505729, -0.2952755905511810774 ) ) ;
#4375=CARTESIAN_POINT ( 'NONE',  ( 0.3391892065151629332, 0.1136516277932330399, -0.2952755905511810774 ) ) ;
#4377=CARTESIAN_POINT ( 'NONE',  ( 0.3496875272944829360, 0.3447318307381752600, -0.006541864722391422388 ) ) ;
#4378=ORIENTED_EDGE ( 'NONE', *, *, #2754, .T. ) ;
#4387=EDGE_CURVE ( 'NONE', #614, #5178, #2538, .T. ) ;
#4405=B_SPLINE_CURVE_WITH_KNOTS ( 'NONE', 3,
 ( #6980, #537, #502, #5805, #4040, #7506, #6373, #3468, #1591, #4684 ),
 .UNSPECIFIED., .F., .F.,
 ( 4, 2, 2, 2, 4 ),
 ( 6.564673817405236669E-19, 0.002239656411828510989, 0.004479312823657021110, 0.006718969235485531231, 0.008958625647314040485 ),
 .UNSPECIFIED. ) ;
#4422=DIRECTION ( 'NONE',  ( 0.000000000000000000, 0.000000000000000000, -1.000000000000000000 ) ) ;
#4438=ORIENTED_EDGE ( 'NONE', *, *, #6603, .F. ) ;
#4439=CARTESIAN_POINT ( 'NONE',  ( 0.000000000000000000, 0.2557161625347750267, 0.1476377952755908163 ) ) ;
#4445=CARTESIAN_POINT ( 'NONE',  ( 0.3585569128062319200, 0.3496569568119790028, 0.001755940978325809575 ) ) ;
#4454=( BOUNDED_SURFACE ( )  B_SPLINE_SURFACE ( 3, 2, ( 
 ( #7162, #1932, #6600 ),
 ( #932, #6745, #3923 ),
 ( #7424, #2196, #407 ),
 ( #6142, #3877, #1532 ),
 ( #366, #1130, #3261 ),
 ( #7390, #6386, #2160 ),
 ( #6251, #6213, #1575 ),
 ( #4377, #2766, #4528 ) ),
 .UNSPECIFIED., .F., .F., .F. ) 
 B_SPLINE_SURFACE_WITH_KNOTS ( ( 4, 2, 2, 4 ),
 ( 3, 3 ),
 ( 0.03551798592901333346, 0.03994769179990642627, 0.04216254473535296921, 0.04437739767079951908 ),
 ( 0.000000000000000000, 1.000000000000000000 ),
 .UNSPECIFIED. ) 
 GEOMETRIC_REPRESENTATION_ITEM ( )  RATIONAL_B_SPLINE_SURFACE ( (
 ( 1.000000000000000000, 0.8047781103519391355, 1.000000000000000000),
 ( 1.000000000000000000, 0.8123785826169017676, 1.000000000000000000),
 ( 1.000000000000000000, 0.8190671539036440407, 1.000000000000000000),
 ( 1.000000000000000000, 0.8191932076449144340, 1.000000000000000000),
 ( 1.000000000000000000, 0.8176085094066379844, 1.000000000000000000),
 ( 1.000000000000000000, 0.8122955484014008354, 1.000000000000000000),
 ( 1.000000000000000000, 0.8086308001280846369, 1.000000000000000000),
 ( 1.000000000000000000, 0.8047712537969720081, 1.000000000000000000) ) ) 
 REPRESENTATION_ITEM ( '' )  SURFACE ( )  );
#4470=CARTESIAN_POINT ( 'NONE',  ( 0.3487102105009278197, -0.2024297391849458061, 0.2527898980517221394 ) ) ;
#4473=CARTESIAN_POINT ( 'NONE',  ( 0.4685039370078740717, -0.3409548833797009237, 0.000000000000000000 ) ) ;
#4478=VERTEX_POINT ( 'NONE', #2821 ) ;
#4483=ORIENTED_EDGE ( 'NONE', *, *, #1153, .T. ) ;
#4484=CARTESIAN_POINT ( 'NONE',  ( 0.000000000000000000, 0.2557161625347750267, 0.1476377952755908163 ) ) ;
#4485=CARTESIAN_POINT ( 'NONE',  ( 0.3528971332113846615, 0.1886393090946605622, 0.2768874834731247514 ) ) ;
#4494=ORIENTED_EDGE ( 'NONE', *, *, #6125, .T. ) ;
#4495=FACE_OUTER_BOUND ( 'NONE', #3281, .T. ) ;
#4504=B_SPLINE_CURVE_WITH_KNOTS ( 'NONE', 3,
 ( #1649, #7380, #5604, #2190, #2796, #2151, #7342, #6854, #4485, #3956 ),
 .UNSPECIFIED., .F., .F.,
 ( 4, 2, 2, 2, 4 ),
 ( 0.000000000000000000, 0.002239656411828510555, 0.004479312823657022845, 0.006718969235485534701, 0.008958625647314047424 ),
 .UNSPECIFIED. ) ;
#4507=CARTESIAN_POINT ( 'NONE',  ( 0.3496779274129794279, -0.3447056852546012129, -0.006496579416451788574 ) ) ;
#4513=CARTESIAN_POINT ( 'NONE',  ( 0.3432736861146659657, 0.1420645347415416815, 0.2952755905511811330 ) ) ;
#4521=ORIENTED_EDGE ( 'NONE', *, *, #1877, .T. ) ;
#4528=CARTESIAN_POINT ( 'NONE',  ( 0.3585665126877356501, 0.3496831043983829046, -0.001800812819183686539 ) ) ;
#4531=DIRECTION ( 'NONE',  ( 0.000000000000000000, 0.000000000000000000, 1.000000000000000000 ) ) ;
#4543=CARTESIAN_POINT ( 'NONE',  ( 0.3585665126877354281, -0.1732820025503174766, 0.3037348580927970443 ) ) ;
#4560=ORIENTED_EDGE ( 'NONE', *, *, #1154, .F. ) ;
#4564=EDGE_LOOP ( 'NONE', ( #232, #5758, #6881, #4853, #3654, #3410, #924 ) ) ;
#4569=PLANE ( 'NONE',  #5141 ) ;
#4570=VERTEX_POINT ( 'NONE', #3546 ) ;
#4578=DIRECTION ( 'NONE',  ( -1.000000000000000000, -0.000000000000000000, -0.000000000000000000 ) ) ;
#4582=CARTESIAN_POINT ( 'NONE',  ( 0.3527006543068525457, -0.1709223289430796822, -0.2960461578774135627 ) ) ;
#4584=UNCERTAINTY_MEASURE_WITH_UNIT (LENGTH_MEASURE( 1.000000000000000082E-05 ), #6521, 'distance_accuracy_value', 'NONE');
#4590=EDGE_CURVE ( 'NONE', #6581, #2461, #715, .T. ) ;
#4594=CARTESIAN_POINT ( 'NONE',  ( 0.3531511627980760681, 0.1878266560944092389, -0.2783075040405467715 ) ) ;
#4595=ADVANCED_FACE ( 'NONE', ( #1741 ), #351, .T. ) ;
#4613=AXIS2_PLACEMENT_3D ( 'NONE', #2859, #1280, #542 ) ;
#4620=EDGE_LOOP ( 'NONE', ( #5185, #2424, #6394, #5371, #3683 ) ) ;
#4635=ADVANCED_FACE ( 'NONE', ( #4200 ), #6538, .F. ) ;
#4637=AXIS2_PLACEMENT_3D ( 'NONE', #7356, #5545, #1977 ) ;
#4648=CARTESIAN_POINT ( 'NONE',  ( 0.3321025531238107620, -0.02909241602403181068, -0.2952755905511810774 ) ) ;
#4659=EDGE_LOOP ( 'NONE', ( #3531, #608, #5023, #6094 ) ) ;
#4663=DIRECTION ( 'NONE',  ( -1.000000000000000000, -0.000000000000000000, -0.000000000000000000 ) ) ;
#4665=ORIENTED_EDGE ( 'NONE', *, *, #1471, .T. ) ;
#4666=CARTESIAN_POINT ( 'NONE',  ( 0.3485616995351332181, -0.1165012447190267864, -0.3017003685801735724 ) ) ;
#4684=CARTESIAN_POINT ( 'NONE',  ( 0.3581828924050324825, -0.1743168766271116221, -0.3019256869348722061 ) ) ;
#4694=FACE_OUTER_BOUND ( 'NONE', #1335, .T. ) ;
#4701=CARTESIAN_POINT ( 'NONE',  ( 0.4685039370078740717, 0.1704774416898499345, 0.2952755905511810774 ) ) ;
#4709=CARTESIAN_POINT ( 'NONE',  ( 8.136851934253910637E-18, -0.02882762270234999827, 0.2952755905511811330 ) ) ;
#4713=FACE_OUTER_BOUND ( 'NONE', #5449, .T. ) ;
#4720=CYLINDRICAL_SURFACE ( 'NONE', #5634, 0.2362204724409449064 ) ;
#4723=CARTESIAN_POINT ( 'NONE',  ( 0.3487105584742864473, -0.1177098269287414900, -0.3017042544367490309 ) ) ;
#4734=VERTEX_POINT ( 'NONE', #6081 ) ;
#4737=ORIENTED_EDGE ( 'NONE', *, *, #427, .F. ) ;
#4745=ORIENTED_EDGE ( 'NONE', *, *, #49, .T. ) ;
#4748=AXIS2_PLACEMENT_3D ( 'NONE', #1138, #1884, #7035 ) ;
#4752=CARTESIAN_POINT ( 'NONE',  ( 0.3459468362671123676, -0.1200707489736706907, 0.2952755905511811885 ) ) ;
#4756=ORIENTED_EDGE ( 'NONE', *, *, #1290, .T. ) ;
#4757=B_SPLINE_CURVE_WITH_KNOTS ( 'NONE', 3,
 ( #5381, #3115, #2019, #222, #7133, #4923 ),
 .UNSPECIFIED., .F., .F.,
 ( 4, 2, 4 ),
 ( 0.004466737480205778058, 0.006712681563759909271, 0.008958625647314040485 ),
 .UNSPECIFIED. ) ;
#4765=CARTESIAN_POINT ( 'NONE',  ( 0.3496779450092586949, 0.1779791412978203036, -0.2952755905511810774 ) ) ;
#4772=CARTESIAN_POINT ( 'NONE',  ( 0.004822332172886149328, 0.2917300191221098293, 0.08525996588982816260 ) ) ;
#4801=CARTESIAN_POINT ( 'NONE',  ( 0.3425764178929368020, -0.2322094954269898481, 0.2008802154383053373 ) ) ;
#4830=CARTESIAN_POINT ( 'NONE',  ( 0.3510872220067592364, -0.3295092824291515621, -0.01982436236955561690 ) ) ;
#4832=CARTESIAN_POINT ( 'NONE',  ( 0.3322368487464851805, -0.06186759433717738121, 0.2952755905511811330 ) ) ;
#4834=FACE_OUTER_BOUND ( 'NONE', #3733, .T. ) ;
#4842=DIRECTION ( 'NONE',  ( -1.000000000000000000, -0.000000000000000000, -0.000000000000000000 ) ) ;
#4845=CARTESIAN_POINT ( 'NONE',  ( 0.000000000000000000, 0.2557161625347750267, 0.1476377952755908163 ) ) ;
#4850=CARTESIAN_POINT ( 'NONE',  ( 0.3336175750056032951, -0.2273032555864670234, 0.1968503937007874682 ) ) ;
#4853=ORIENTED_EDGE ( 'NONE', *, *, #1975, .F. ) ;
#4870=CONICAL_SURFACE ( 'NONE', #3896, 0.2952755905511810774, 1.047197551196600518 ) ;
#4878=VERTEX_POINT ( 'NONE', #3318 ) ;
#4879=CARTESIAN_POINT ( 'NONE',  ( 0.000000000000000000, 0.000000000000000000, 0.000000000000000000 ) ) ;
#4890=DIRECTION ( 'NONE',  ( 0.3420201433256623291, 0.000000000000000000, -0.9396926207859106484 ) ) ;
#4892=CARTESIAN_POINT ( 'NONE',  ( 0.3306743754077736130, -0.2557161625347754708, 0.1476377952755905387 ) ) ;
#4899=CARTESIAN_POINT ( 'NONE',  ( 0.3426144402833972147, 0.2318662757222082205, -0.2014770286013785050 ) ) ;
#4912=EDGE_LOOP ( 'NONE', ( #4745, #7042, #3924, #1613 ) ) ;
#4920=CARTESIAN_POINT ( 'NONE',  ( 0.01834252172841625839, 0.1843865549457985864, -0.2711842997036481573 ) ) ;
#4923=CARTESIAN_POINT ( 'NONE',  ( 0.3581828924050323715, 0.1743168766271107895, -0.3019256869348722061 ) ) ;
#4927=CARTESIAN_POINT ( 'NONE',  ( 0.02637295201093722841, 0.3409548833797004797, 3.882420715168025960E-18 ) ) ;
#4935=EDGE_LOOP ( 'NONE', ( #4014, #1038, #4494, #2980 ) ) ;
#4936=CARTESIAN_POINT ( 'NONE',  ( -1.678725927747302331E-16, 0.2411939993270974525, 0.1727909197870958202 ) ) ;
#4941=ORIENTED_EDGE ( 'NONE', *, *, #1639, .T. ) ;
#4948=CARTESIAN_POINT ( 'NONE',  ( 0.003035684155427232581, -0.2268414356900468332, 0.1976502892253331478 ) ) ;
#4951=ORIENTED_EDGE ( 'NONE', *, *, #7243, .T. ) ;
#4954=B_SPLINE_CURVE_WITH_KNOTS ( 'NONE', 3,
 ( #1158, #1904, #4234, #3474, #568, #2884, #5231, #2042, #2314 ),
 .UNSPECIFIED., .F., .F.,
 ( 4, 2, 1, 2, 4 ),
 ( 0.000000000000000000, 0.002165063509461098365, 0.004330127018922196730, 0.006495190528383293360, 0.008660254037844391725 ),
 .UNSPECIFIED. ) ;
#4955=ADVANCED_FACE ( 'NONE', ( #6407 ), #5261, .F. ) ;
#4962=ADVANCED_FACE ( 'NONE', ( #1666 ), #2832, .T. ) ;
#4966=CARTESIAN_POINT ( 'NONE',  ( 0.3336175750056031841, 0.2273032555864666071, -0.1968503937007874127 ) ) ;
#4984=CARTESIAN_POINT ( 'NONE',  ( -5.972582710757682675E-17, -0.2484822268960368286, 0.1601673393405688428 ) ) ;
#5019=MECHANICAL_DESIGN_GEOMETRIC_PRESENTATION_REPRESENTATION('',(#6717),#507);
#5023=ORIENTED_EDGE ( 'NONE', *, *, #3118, .T. ) ;
#5029=CARTESIAN_POINT ( 'NONE',  ( 0.3483227611829846082, 0.1704774416898497680, -0.2952755905511810774 ) ) ;
#5036=CARTESIAN_POINT ( 'NONE',  ( 2.989606299212598017, 0.000000000000000000, 0.000000000000000000 ) ) ;
#5047=CARTESIAN_POINT ( 'NONE',  ( -6.322734125961233610E-17, -0.2702383257424528229, 0.1224846707640861176 ) ) ;
#5048=CARTESIAN_POINT ( 'NONE',  ( 0.3496875272944827695, -0.1667004943313752652, 0.3018174552735723437 ) ) ;
#5057=ORIENTED_EDGE ( 'NONE', *, *, #51, .F. ) ;
#5077=DIRECTION ( 'NONE',  ( 0.000000000000000000, 0.000000000000000000, 1.000000000000000000 ) ) ;
#5086=ORIENTED_EDGE ( 'NONE', *, *, #249, .F. ) ;
#5098=CARTESIAN_POINT ( 'NONE',  ( 0.0006233585804810778822, -0.2702164766613439628, -0.1225225144826657953 ) ) ;
#5115=CARTESIAN_POINT ( 'NONE',  ( 0.4330708661417324024, 0.000000000000000000, 0.000000000000000000 ) ) ;
#5124=CARTESIAN_POINT ( 'NONE',  ( 0.3565422270302656127, -0.1673297761639321035, 0.3007275071673038980 ) ) ;
#5137=CARTESIAN_POINT ( 'NONE',  ( 0.3585665126877354281, 0.1732820025503171713, -0.3037348580927971553 ) ) ;
#5141=AXIS2_PLACEMENT_3D ( 'NONE', #3422, #905, #6751 ) ;
#5144=ORIENTED_EDGE ( 'NONE', *, *, #3092, .F. ) ;
#5145=CARTESIAN_POINT ( 'NONE',  ( 0.3574299024618896037, 0.1732824651941676231, 0.3001340337771135625 ) ) ;
#5150=EDGE_CURVE ( 'NONE', #2222, #1896, #87, .T. ) ;
#5152=DIRECTION ( 'NONE',  ( -1.000000000000000000, -0.000000000000000000, 0.000000000000000000 ) ) ;
#5154=CARTESIAN_POINT ( 'NONE',  ( 0.4685039370078740717, -0.1704774416898499345, 0.2952755905511811330 ) ) ;
#5161=EDGE_CURVE ( 'NONE', #2401, #3022, #6933, .T. ) ;
#5166=AXIS2_PLACEMENT_3D ( 'NONE', #418, #2134, #2741 ) ;
#5178=VERTEX_POINT ( 'NONE', #1106 ) ;
#5185=ORIENTED_EDGE ( 'NONE', *, *, #1153, .F. ) ;
#5187=FACE_BOUND ( 'NONE', #7399, .T. ) ;
#5193=DIRECTION ( 'NONE',  ( -1.000000000000000000, -0.000000000000000000, -0.000000000000000000 ) ) ;
#5203=DIRECTION ( 'NONE',  ( 1.000000000000000000, 0.000000000000000000, 0.000000000000000000 ) ) ;
#5211=VERTEX_POINT ( 'NONE', #4025 ) ;
#5217=ORIENTED_EDGE ( 'NONE', *, *, #7389, .T. ) ;
#5225=DIRECTION ( 'NONE',  ( 0.000000000000000000, 0.5000000000000008882, -0.8660254037844380415 ) ) ;
#5227=LINE ( 'NONE', #4150, #526 ) ;
#5231=CARTESIAN_POINT ( 'NONE',  ( 0.3391892065151629332, 0.3125419764313920323, 0.04921259842519686012 ) ) ;
#5234=CARTESIAN_POINT ( 'NONE',  ( 0.3505602286436571013, -0.1704774416898497957, 0.2952755905511814660 ) ) ;
#5249=CARTESIAN_POINT ( 'NONE',  ( 0.3528822938286764188, -0.1453909600788099998, 0.3018098512751525853 ) ) ;
#5255=CARTESIAN_POINT ( 'NONE',  ( 0.3496875412996344190, 0.1780314126850971457, 0.2952755905511810774 ) ) ;
#5260=CARTESIAN_POINT ( 'NONE',  ( 0.3505601438611540277, -0.1704774416898505729, -0.2952755905511810774 ) ) ;
#5261=PLANE ( 'NONE',  #1359 ) ;
#5279=CARTESIAN_POINT ( 'NONE',  ( 0.3410249605999410294, -1.062517223525361548E-12, -0.3014927230551905368 ) ) ;
#5291=CARTESIAN_POINT ( 'NONE',  ( 0.002479217192759452203, -0.05744896992506681732, 0.2952755905511810774 ) ) ;
#5303=AXIS2_PLACEMENT_3D ( 'NONE', #5036, #2201, #4531 ) ;
#5319=B_SPLINE_CURVE_WITH_KNOTS ( 'NONE', 3,
 ( #6537, #5469, #4318, #265, #7137, #1279, #5968, #228, #6574 ),
 .UNSPECIFIED., .F., .F.,
 ( 4, 2, 1, 2, 4 ),
 ( 0.000000000000000000, 0.002165063509461096630, 0.004330127018922193260, 0.006495190528383289023, 0.008660254037844388256 ),
 .UNSPECIFIED. ) ;
#5320=ORIENTED_EDGE ( 'NONE', *, *, #7091, .T. ) ;
#5322=CARTESIAN_POINT ( 'NONE',  ( 0.3459463601586513781, -0.1956820507697304701, -0.2516199270400212851 ) ) ;
#5333=ORIENTED_EDGE ( 'NONE', *, *, #3644, .T. ) ;
#5338=CARTESIAN_POINT ( 'NONE',  ( 0.3403868552871069930, -0.05881191477760600722, -0.2952755905511810774 ) ) ;
#5347=CARTESIAN_POINT ( 'NONE',  ( 0.3483227611829848303, 0.3409548833797004797, 0.000000000000000000 ) ) ;
#5349=ORIENTED_EDGE ( 'NONE', *, *, #3893, .T. ) ;
#5358=ORIENTED_EDGE ( 'NONE', *, *, #5161, .F. ) ;
#5360=DIRECTION ( 'NONE',  ( 0.000000000000000000, 1.000000000000000000, -1.001543065824774208E-16 ) ) ;
#5368=CARTESIAN_POINT ( 'NONE',  ( 0.4685039370078740717, 0.3409548833797004797, 0.000000000000000000 ) ) ;
#5371=ORIENTED_EDGE ( 'NONE', *, *, #842, .F. ) ;
#5379=DIRECTION ( 'NONE',  ( 0.000000000000000000, 0.000000000000000000, 1.000000000000000000 ) ) ;
#5381=CARTESIAN_POINT ( 'NONE',  ( 0.3410249605999410294, -1.062517223525361548E-12, -0.3014927230551905368 ) ) ;
#5384=DIRECTION ( 'NONE',  ( -0.7071067811865496822, 8.659560562354906974E-17, -0.7071067811865453523 ) ) ;
#5399=ORIENTED_EDGE ( 'NONE', *, *, #5938, .T. ) ;
#5407=AXIS2_PLACEMENT_3D ( 'NONE', #7169, #2546, #6572 ) ;
#5416=FACE_OUTER_BOUND ( 'NONE', #1035, .T. ) ;
#5417=ORIENTED_EDGE ( 'NONE', *, *, #1486, .T. ) ;
#5419=EDGE_LOOP ( 'NONE', ( #974, #3759, #2679, #902, #5785 ) ) ;
#5421=SHAPE_REPRESENTATION_RELATIONSHIP ( 'NONE' , 'NONE' ,  #1552, #6318 ) ;
#5429=CARTESIAN_POINT ( 'NONE',  ( 0.000000000000000000, 0.000000000000000000, 0.000000000000000000 ) ) ;
#5431=EDGE_CURVE ( 'NONE', #698, #5178, #734, .T. ) ;
#5432=EDGE_CURVE ( 'NONE', #5600, #6027, #3194, .T. ) ;
#5440=ADVANCED_FACE ( 'NONE', ( #3020 ), #2368, .F. ) ;
#5448=CARTESIAN_POINT ( 'NONE',  ( 0.3479980290964227452, 0.3208941761715193852, -0.04760384692076755769 ) ) ;
#5449=EDGE_LOOP ( 'NONE', ( #7363, #2970, #553, #7089, #3457, #2771 ) ) ;
#5450=ORIENTED_EDGE ( 'NONE', *, *, #4387, .F. ) ;
#5464=FACE_OUTER_BOUND ( 'NONE', #7391, .T. ) ;
#5469=CARTESIAN_POINT ( 'NONE',  ( 0.3432736861146661322, -0.1846838951640047688, -0.2706692913385826404 ) ) ;
#5472=DIRECTION ( 'NONE',  ( 1.000000000000000000, 0.000000000000000000, 0.000000000000000000 ) ) ;
#5482=B_SPLINE_CURVE_WITH_KNOTS ( 'NONE', 3,
 ( #3065, #3028, #3492, #5291, #4709, #4181 ),
 .UNSPECIFIED., .F., .F.,
 ( 4, 2, 4 ),
 ( 0.007897041933671775787, 0.01008815886328916570, 0.01227927579290655560 ),
 .UNSPECIFIED. ) ;
#5497=CARTESIAN_POINT ( 'NONE',  ( 0.3391892065151629332, -0.1136516277932338725, -0.2952755905511810774 ) ) ;
#5502=( NAMED_UNIT ( * ) SI_UNIT ( $, .STERADIAN. ) SOLID_ANGLE_UNIT ( ) );
#5545=DIRECTION ( 'NONE',  ( 1.000000000000000000, 0.000000000000000000, -0.000000000000000000 ) ) ;
#5550=CARTESIAN_POINT ( 'NONE',  ( 0.01832242175888482497, -0.3270109559553083245, 0.02415159075610082487 ) ) ;
#5553=ORIENTED_EDGE ( 'NONE', *, *, #3644, .F. ) ;
#5557=CARTESIAN_POINT ( 'NONE',  ( 0.02637295201093703412, 0.1704774416898499345, 0.2952755905511810774 ) ) ;
#5564=ADVANCED_FACE ( 'NONE', ( #4285 ), #2335, .F. ) ;
#5565=VERTEX_POINT ( 'NONE', #999 ) ;
#5571=CARTESIAN_POINT ( 'NONE',  ( 0.3527008206095850751, 0.3418447298186451655, 4.692841048826145323E-17 ) ) ;
#5581=CARTESIAN_POINT ( 'NONE',  ( 0.003035684155427062578, 0.2268414356900468054, -0.1976502892253328703 ) ) ;
#5583=B_SPLINE_CURVE_WITH_KNOTS ( 'NONE', 3,
 ( #77, #4126, #2559, #2403, #6461, #121 ),
 .UNSPECIFIED., .F., .F.,
 ( 4, 2, 4 ),
 ( 0.000000000000000000, 0.002233368740102886427, 0.004466737480205772853 ),
 .UNSPECIFIED. ) ;
#5588=CARTESIAN_POINT ( 'NONE',  ( 0.3510872220068100846, -0.1819230426404178091, 0.2754512281816298147 ) ) ;
#5596=PRODUCT_CONTEXT ( 'NONE', #3255, 'mechanical' ) ;
#5597=DIRECTION ( 'NONE',  ( -0.000000000000000000, 0.000000000000000000, 1.000000000000000000 ) ) ;
#5600=VERTEX_POINT ( 'NONE', #6314 ) ;
#5602=ORIENTED_EDGE ( 'NONE', *, *, #2255, .T. ) ;
#5604=CARTESIAN_POINT ( 'NONE',  ( 0.3485373078438442351, 0.3194486952732363827, 0.05009812457233156491 ) ) ;
#5608=ORIENTED_EDGE ( 'NONE', *, *, #1349, .F. ) ;
#5613=EDGE_LOOP ( 'NONE', ( #5602, #6514, #5320 ) ) ;
#5615=CARTESIAN_POINT ( 'NONE',  ( 0.002549129251883240199, 0.05807386165065146072, -0.2952755905511810219 ) ) ;
#5623=AXIS2_PLACEMENT_3D ( 'NONE', #2484, #158, #3123 ) ;
#5626=AXIS2_PLACEMENT_3D ( 'NONE', #560, #4578, #6438 ) ;
#5632=VERTEX_POINT ( 'NONE', #610 ) ;
#5634=AXIS2_PLACEMENT_3D ( 'NONE', #713, #2999, #5379 ) ;
#5637=CARTESIAN_POINT ( 'NONE',  ( 0.3574269917172681610, 0.1732784665916975442, -0.3001271079942677833 ) ) ;
#5651=ORIENTED_EDGE ( 'NONE', *, *, #2978, .T. ) ;
#5653=ORIENTED_EDGE ( 'NONE', *, *, #1975, .T. ) ;
#5665=CARTESIAN_POINT ( 'NONE',  ( 0.3432736861146661322, 0.3267484299055462005, -0.02460629921259842659 ) ) ;
#5689=ORIENTED_EDGE ( 'NONE', *, *, #5432, .T. ) ;
#5695=CARTESIAN_POINT ( 'NONE',  ( 0.3581828924050323715, -0.1743168766271109560, 0.3019256869348722616 ) ) ;
#5699=DIRECTION ( 'NONE',  ( -1.000000000000000000, -0.000000000000000000, -0.000000000000000000 ) ) ;
#5704=CARTESIAN_POINT ( 'NONE',  ( 0.4685039370078740717, 0.1704774416898497680, -0.2952755905511810774 ) ) ;
#5706=LINE ( 'NONE', #7478, #5770 ) ;
#5724=ADVANCED_FACE ( 'NONE', ( #4694 ), #1244, .F. ) ;
#5730=LINE ( 'NONE', #5154, #7222 ) ;
#5758=ORIENTED_EDGE ( 'NONE', *, *, #943, .T. ) ;
#5765=CARTESIAN_POINT ( 'NONE',  ( 0.3574269917172687161, -0.3465569331832414335, -9.402262055513304185E-15 ) ) ;
#5770=VECTOR ( 'NONE', #6802, 39.37007874015748143 ) ;
#5778=DIRECTION ( 'NONE',  ( 0.000000000000000000, 0.000000000000000000, 1.000000000000000000 ) ) ;
#5785=ORIENTED_EDGE ( 'NONE', *, *, #5432, .F. ) ;
#5792=CARTESIAN_POINT ( 'NONE',  ( 0.3426147637089221321, -0.05832033309504448121, 0.3015404986019939448 ) ) ;
#5796=DIRECTION ( 'NONE',  ( -1.000000000000000000, -0.000000000000000000, -0.000000000000000000 ) ) ;
#5799=CIRCLE ( 'NONE', #663, 0.4507874015748032370 ) ;
#5801=EDGE_CURVE ( 'NONE', #7420, #6581, #2030, .T. ) ;
#5805=CARTESIAN_POINT ( 'NONE',  ( 0.3425764178929370796, -0.2900721174007588332, -0.1006592143205869427 ) ) ;
#5810=CARTESIAN_POINT ( 'NONE',  ( 0.3336175750056032396, -0.05682581389661664484, 0.2952755905511811330 ) ) ;
#5812=CARTESIAN_POINT ( 'NONE',  ( 0.002513486811083437498, 0.2845799557467908469, -0.09764423893321776127 ) ) ;
#5824=B_SPLINE_CURVE_WITH_KNOTS ( 'NONE', 3,
 ( #7220, #5637, #3131, #7367, #2597, #7328 ),
 .UNSPECIFIED., .F., .F.,
 ( 4, 2, 4 ),
 ( -3.269571951033989319E-06, 0.0001651384380483822119, 0.0003335464480477984012 ),
 .UNSPECIFIED. ) ;
#5829=CARTESIAN_POINT ( 'NONE',  ( 0.3483227611829846637, 0.1704774416898499345, 0.2952755905511810774 ) ) ;
#5836=CARTESIAN_POINT ( 'NONE',  ( 0.3483227611829848303, -0.1704774416898505729, -0.2952755905511810774 ) ) ;
#5846=DIRECTION ( 'NONE',  ( 0.000000000000000000, 0.000000000000000000, -1.000000000000000000 ) ) ;
#5852=CONICAL_SURFACE ( 'NONE', #5623, 0.4629062255509093782, 1.221730476396037490 ) ;
#5859=CARTESIAN_POINT ( 'NONE',  ( 0.3581828924050324825, -0.1743168766271116221, -0.3019256869348722061 ) ) ;
#5867=CARTESIAN_POINT ( 'NONE',  ( 0.3496779098333545610, -0.1779789496721726760, 0.2952755905511811330 ) ) ;
#5877=CARTESIAN_POINT ( 'NONE',  ( 0.3496875133419357629, -0.1780312604149854316, -0.2952755905511810774 ) ) ;
#5888=DIRECTION ( 'NONE',  ( 0.000000000000000000, -0.8660254037844379305, 0.5000000000000013323 ) ) ;
#5897=EDGE_CURVE ( 'NONE', #7420, #450, #506, .T. ) ;
#5903=CARTESIAN_POINT ( 'NONE',  ( 0.3528971332113847725, 0.3341112492250003507, -0.02492269209175868722 ) ) ;
#5907=CARTESIAN_POINT ( 'NONE',  ( 0.3465694189147311421, -0.3147628225698668736, -0.04536598007755129891 ) ) ;
#5922=AXIS2_PLACEMENT_3D ( 'NONE', #1727, #4065, #2303 ) ;
#5927=CARTESIAN_POINT ( 'NONE',  ( -1.704737175733852238E-16, 0.2629500981735131693, 0.1351082512106132616 ) ) ;
#5938=EDGE_CURVE ( 'NONE', #7488, #2228, #5706, .T. ) ;
#5948=CARTESIAN_POINT ( 'NONE',  ( 0.3426404862726871725, 0.2904653615686527135, -0.09998168480679492376 ) ) ;
#5966=B_SPLINE_CURVE_WITH_KNOTS ( 'NONE', 3,
 ( #4845, #5927, #2589, #1321, #4772, #684, #759, #4927 ),
 .UNSPECIFIED., .F., .F.,
 ( 4, 2, 2, 4 ),
 ( 0.004381617662950689981, 0.005472867551409524994, 0.006564117439868360007, 0.008746617216786028298 ),
 .UNSPECIFIED. ) ;
#5968=CARTESIAN_POINT ( 'NONE',  ( 0.3391892065151630442, -0.3125419764313924764, -0.04921259842519686706 ) ) ;
#5982=PRODUCT_DEFINITION ( 'UNKNOWN', '', #2273, #3041 ) ;
#5987=SHAPE_DEFINITION_REPRESENTATION ( #72, #1552 ) ;
#5992=CARTESIAN_POINT ( 'NONE',  ( 0.3483227611829846637, -0.1704774416898499345, 0.2952755905511811330 ) ) ;
#6010=PRODUCT ( 'hex flange bolt small_iso_ISO 4162 - M12 x 65 x 65-N', 'hex flange bolt small_iso_ISO 4162 - M12 x 65 x 65-N', '', ( #5596 ) ) ;
#6015=VECTOR ( 'NONE', #5699, 39.37007874015748143 ) ;
#6017=FACE_OUTER_BOUND ( 'NONE', #3680, .T. ) ;
#6018=AXIS2_PLACEMENT_3D ( 'NONE', #6479, #2422, #1733 ) ;
#6024=CARTESIAN_POINT ( 'NONE',  ( 0.3565325103478086954, -0.1673557731150450700, -0.3006824791271353603 ) ) ;
#6027=VERTEX_POINT ( 'NONE', #7440 ) ;
#6032=CARTESIAN_POINT ( 'NONE',  ( 0.3426404862726872280, -0.2904653615686530466, 0.09998168480679490988 ) ) ;
#6045=CARTESIAN_POINT ( 'NONE',  ( 0.000000000000000000, -0.2557161625347750822, -0.1476377952755907330 ) ) ;
#6048=CARTESIAN_POINT ( 'NONE',  ( 0.3581828924050323715, -0.1743168766271109560, 0.3019256869348722616 ) ) ;
#6052=VECTOR ( 'NONE', #5384, 39.37007874015748143 ) ;
#6060=CARTESIAN_POINT ( 'NONE',  ( 1.170506159394721758E-17, 0.02884736746562922144, 0.2952755905511810774 ) ) ;
#6064=CARTESIAN_POINT ( 'NONE',  ( 0.3487102105009288744, -0.3201373431253433655, -0.04891434758976972302 ) ) ;
#6079=FACE_OUTER_BOUND ( 'NONE', #6823, .T. ) ;
#6081=CARTESIAN_POINT ( 'NONE',  ( 0.02637295201093697167, 0.1704774416898497680, -0.2952755905511810774 ) ) ;
#6091=FACE_OUTER_BOUND ( 'NONE', #6959, .T. ) ;
#6092=ADVANCED_FACE ( 'NONE', ( #3470 ), #579, .F. ) ;
#6094=ORIENTED_EDGE ( 'NONE', *, *, #7243, .F. ) ;
#6101=CARTESIAN_POINT ( 'NONE',  ( 0.004822332172886236931, -0.2197023059474404461, 0.2100156246613535393 ) ) ;
#6104=CARTESIAN_POINT ( 'NONE',  ( 0.3505602286436571569, 0.3409548833797004797, 4.673058124370679309E-18 ) ) ;
#6105=CARTESIAN_POINT ( 'NONE',  ( 0.3410076799406686066, -0.2467857494855110190, 0.1755389823809323790 ) ) ;
#6106=AXIS2_PLACEMENT_3D ( 'NONE', #1821, #3087, #3009 ) ;
#6111=CIRCLE ( 'NONE', #4637, 0.2952755905511810774 ) ;
#6113=DIRECTION ( 'NONE',  ( 0.000000000000000000, 0.000000000000000000, -1.000000000000000000 ) ) ;
#6122=DIRECTION ( 'NONE',  ( 0.000000000000000000, 0.000000000000000000, -1.000000000000000000 ) ) ;
#6125=EDGE_CURVE ( 'NONE', #2228, #5565, #5227, .T. ) ;
#6132=CARTESIAN_POINT ( 'NONE',  ( 0.01834252172841674411, -0.3270457701237520221, -0.02409129084753309710 ) ) ;
#6135=CARTESIAN_POINT ( 'NONE',  ( 0.02637295201093707228, -0.1704774416898499345, 0.2952755905511811330 ) ) ;
#6139=CARTESIAN_POINT ( 'NONE',  ( 0.3432736861146661878, -0.1420645347415422088, -0.2952755905511810774 ) ) ;
#6142=CARTESIAN_POINT ( 'NONE',  ( 0.3321022367506963890, 0.2702568778840441777, 0.1224525375122600818 ) ) ;
#6155=CARTESIAN_POINT ( 'NONE',  ( 0.3483227611829848303, 0.3409548833797004797, 0.000000000000000000 ) ) ;
#6171=EDGE_CURVE ( 'NONE', #6027, #4478, #4757, .T. ) ;
#6174=ORIENTED_EDGE ( 'NONE', *, *, #51, .T. ) ;
#6179=ADVANCED_FACE ( 'NONE', ( #5464 ), #7480, .T. ) ;
#6213=CARTESIAN_POINT ( 'NONE',  ( 0.3510872220067180471, 0.3295092824291462330, 0.01982436236955231745 ) ) ;
#6215=CARTESIAN_POINT ( 'NONE',  ( 0.01841426102874111140, 0.1429077274040426171, -0.2952755905511810219 ) ) ;
#6216=AXIS2_PLACEMENT_3D ( 'NONE', #3690, #2500, #4100 ) ;
#6218=CARTESIAN_POINT ( 'NONE',  ( 0.3997746709170348356, 0.000000000000000000, 0.000000000000000000 ) ) ;
#6228=CARTESIAN_POINT ( 'NONE',  ( 0.3442723180357430413, -0.1814473180894617399, 0.2762752072743029363 ) ) ;
#6234=AXIS2_PLACEMENT_3D ( 'NONE', #6218, #3235, #977 ) ;
#6236=CARTESIAN_POINT ( 'NONE',  ( 0.4685039370078740717, 0.1704774416898497680, -0.2952755905511810774 ) ) ;
#6251=CARTESIAN_POINT ( 'NONE',  ( 0.3442723180356496160, 0.3299850069800976948, 0.01900038327686272982 ) ) ;
#6266=CARTESIAN_POINT ( 'NONE',  ( 0.3387177083556423551, -0.2412911239081454440, 0.1726226950780508362 ) ) ;
#6280=ORIENTED_EDGE ( 'NONE', *, *, #3092, .T. ) ;
#6290=CIRCLE ( 'NONE', #2976, 0.2362204724409449064 ) ;
#6303=CARTESIAN_POINT ( 'NONE',  ( 0.3409812221349244332, -0.2467127425962881426, 0.1756638922268692060 ) ) ;
#6313=CARTESIAN_POINT ( 'NONE',  ( 0.000000000000000000, 0.000000000000000000, 0.000000000000000000 ) ) ;
#6314=CARTESIAN_POINT ( 'NONE',  ( 0.3581828924050324825, -0.1743168766271116221, -0.3019256869348722061 ) ) ;
#6318=ADVANCED_BREP_SHAPE_REPRESENTATION ( '', ( #3913, #5166 ), #1726 ) ;
#6328=CARTESIAN_POINT ( 'NONE',  ( 0.4685039370078740717, 0.000000000000000000, 0.000000000000000000 ) ) ;
#6334=FACE_OUTER_BOUND ( 'NONE', #853, .T. ) ;
#6373=CARTESIAN_POINT ( 'NONE',  ( 0.3426404862726872280, -0.2318193597401798645, -0.2015595396344879719 ) ) ;
#6377=CARTESIAN_POINT ( 'NONE',  ( 0.3483227611829846637, 0.1704774416898499345, 0.2952755905511810774 ) ) ;
#6384=DIRECTION ( 'NONE',  ( 0.000000000000000000, -0.5000000000000012212, -0.8660254037844377084 ) ) ;
#6386=CARTESIAN_POINT ( 'NONE',  ( 0.3465694189147047188, 0.3147628225698786419, 0.04536598007754604617 ) ) ;
#6394=ORIENTED_EDGE ( 'NONE', *, *, #5897, .T. ) ;
#6407=FACE_OUTER_BOUND ( 'NONE', #2687, .T. ) ;
#6419=CARTESIAN_POINT ( 'NONE',  ( 0.3997746709170348356, 5.668966274263039413E-17, 0.4629062255509093782 ) ) ;
#6435=CONICAL_SURFACE ( 'NONE', #3142, 0.1982677165354330695, 0.7853981633974452814 ) ;
#6438=DIRECTION ( 'NONE',  ( 0.000000000000000000, 0.000000000000000000, 1.000000000000000000 ) ) ;
#6447=CARTESIAN_POINT ( 'NONE',  ( 0.3426148638729746843, -0.05855635169929876427, -0.3015406112749626777 ) ) ;
#6454=ADVANCED_FACE ( 'NONE', ( #4713 ), #1802, .F. ) ;
#6461=CARTESIAN_POINT ( 'NONE',  ( 0.3410249605999788325, 0.02903799983316233957, 0.3014927230551917026 ) ) ;
#6465=DIRECTION ( 'NONE',  ( 0.000000000000000000, -1.001543065824774208E-16, -1.000000000000000000 ) ) ;
#6473=( NAMED_UNIT ( * ) SI_UNIT ( $, .STERADIAN. ) SOLID_ANGLE_UNIT ( ) );
#6475=CARTESIAN_POINT ( 'NONE',  ( 0.3337350301074833991, 0.05917206666036364110, 0.2952755905511810774 ) ) ;
#6479=CARTESIAN_POINT ( 'NONE',  ( 0.000000000000000000, 0.3409548833797004797, 2.164902785881980513E-17 ) ) ;
#6486=DIRECTION ( 'NONE',  ( 0.000000000000000000, -1.224646799147353700E-16, 1.000000000000000000 ) ) ;
#6489=CARTESIAN_POINT ( 'NONE',  ( 0.3337358785015786533, -0.05918271685993679171, -0.2952755905511810774 ) ) ;
#6514=ORIENTED_EDGE ( 'NONE', *, *, #4351, .T. ) ;
#6521=( CONVERSION_BASED_UNIT ( 'INCH', #2416 ) LENGTH_UNIT ( ) NAMED_UNIT ( #1012 ) );
#6522=CARTESIAN_POINT ( 'NONE',  ( 0.3531509790457915132, 0.1471070558423459573, 0.3018164037399326816 ) ) ;
#6523=CARTESIAN_POINT ( 'NONE',  ( 0.3483227611829846082, 0.1704774416898497680, -0.2952755905511810774 ) ) ;
#6537=CARTESIAN_POINT ( 'NONE',  ( 0.3483227611829848303, -0.1704774416898505729, -0.2952755905511810774 ) ) ;
#6538=PLANE ( 'NONE',  #4613 ) ;
#6539=FACE_OUTER_BOUND ( 'NONE', #4564, .T. ) ;
#6557=CARTESIAN_POINT ( 'NONE',  ( 0.3337354549119980751, -0.2853048623713481113, -0.09638866382874244909 ) ) ;
#6572=DIRECTION ( 'NONE',  ( 0.000000000000000000, 0.000000000000000000, -1.000000000000000000 ) ) ;
#6574=CARTESIAN_POINT ( 'NONE',  ( 0.3483227611829849413, -0.3409548833797009237, 0.000000000000000000 ) ) ;
#6581=VERTEX_POINT ( 'NONE', #5992 ) ;
#6596=CARTESIAN_POINT ( 'NONE',  ( 0.3585665266928871331, 0.1764011776056260972, 0.3019340455778471433 ) ) ;
#6600=CARTESIAN_POINT ( 'NONE',  ( 0.3585569128062318645, 0.1733077889112127901, 0.3036897776982951380 ) ) ;
#6603=EDGE_CURVE ( 'NONE', #2461, #4570, #6763, .T. ) ;
#6608=CARTESIAN_POINT ( 'NONE',  ( 0.01178921041716498620, 0.1149842948508797008, -0.2952755905511810774 ) ) ;
#6628=CARTESIAN_POINT ( 'NONE',  ( 0.3388536909602617997, 0.2864058322153591463, -0.09448172812127442199 ) ) ;
#6638=CARTESIAN_POINT ( 'NONE',  ( 0.3528971332113848836, -0.3341112492250008503, 0.02492269209175877395 ) ) ;
#6645=EDGE_CURVE ( 'NONE', #614, #931, #3057, .T. ) ;
#6646=ADVANCED_FACE ( 'NONE', ( #4834 ), #4454, .F. ) ;
#6656=VECTOR ( 'NONE', #4842, 39.37007874015748143 ) ;
#6661=CARTESIAN_POINT ( 'NONE',  ( -1.320571051624814422E-17, -0.02882762270237488114, -0.2952755905511810219 ) ) ;
#6663=ORIENTED_EDGE ( 'NONE', *, *, #1302, .F. ) ;
#6668=CARTESIAN_POINT ( 'NONE',  ( 0.3442723180356911383, -0.3299850069800938646, -0.01900038327687023423 ) ) ;
#6673=ORIENTED_EDGE ( 'NONE', *, *, #5150, .T. ) ;
#6677=CARTESIAN_POINT ( 'NONE',  ( 0.3581828924050323715, -0.1743168766271109560, 0.3019256869348722616 ) ) ;
#6711=CIRCLE ( 'NONE', #5626, 0.4507874015748032370 ) ;
#6717=STYLED_ITEM('',(#7587),#3913);
#6720=DIRECTION ( 'NONE',  ( -1.000000000000000000, -0.000000000000000000, -0.000000000000000000 ) ) ;
#6734=ORIENTED_EDGE ( 'NONE', *, *, #3118, .F. ) ;
#6739=ORIENTED_EDGE ( 'NONE', *, *, #7514, .F. ) ;
#6741=EDGE_LOOP ( 'NONE', ( #5086, #1174, #5399, #7298 ) ) ;
#6743=CARTESIAN_POINT ( 'NONE',  ( 0.3336175750056032951, -0.05682581389661717219, -0.2952755905511811330 ) ) ;
#6745=CARTESIAN_POINT ( 'NONE',  ( 0.3459463601587901560, 0.1956820507697113742, 0.2516199270399913090 ) ) ;
#6746=ORIENTED_EDGE ( 'NONE', *, *, #3262, .T. ) ;
#6751=DIRECTION ( 'NONE',  ( -0.000000000000000000, 0.000000000000000000, -1.000000000000000000 ) ) ;
#6759=CARTESIAN_POINT ( 'NONE',  ( 0.3391892065151627111, 0.1988903486381581598, -0.2460629921259842312 ) ) ;
#6763=B_SPLINE_CURVE_WITH_KNOTS ( 'NONE', 3,
 ( #6677, #136, #3769, #4801, #6105, #3071, #6032, #1850, #6638, #181 ),
 .UNSPECIFIED., .F., .F.,
 ( 4, 2, 2, 2, 4 ),
 ( 0.000000000000000000, 0.002239656411828512290, 0.004479312823657024580, 0.006718969235485537303, 0.008958625647314049159 ),
 .UNSPECIFIED. ) ;
#6765=CARTESIAN_POINT ( 'NONE',  ( 0.4685039370078740717, 0.000000000000000000, 0.000000000000000000 ) ) ;
#6775=B_SPLINE_CURVE_WITH_KNOTS ( 'NONE', 3,
 ( #4350, #7282, #2061, #4582, #5260, #5836 ),
 .UNSPECIFIED., .F., .F.,
 ( 4, 2, 4 ),
 ( -3.269571951031369869E-06, 0.0001651384380483837840, 0.0003335464480477989433 ),
 .UNSPECIFIED. ) ;
#6778=CARTESIAN_POINT ( 'NONE',  ( 1.068462032678259234E-16, -0.2629500981735136689, -0.1351082512106133171 ) ) ;
#6787=CARTESIAN_POINT ( 'NONE',  ( 0.3581828924050324825, 0.3486337532542225226, 1.056976728655274672E-17 ) ) ;
#6802=DIRECTION ( 'NONE',  ( -0.7071067811865496822, 0.000000000000000000, 0.7071067811865453523 ) ) ;
#6808=CARTESIAN_POINT ( 'NONE',  ( 0.02637295201093723881, -0.1704774416898505729, -0.2952755905511810774 ) ) ;
#6809=CARTESIAN_POINT ( 'NONE',  ( 0.3496875272944827695, 0.1667004943313749321, -0.3018174552735724547 ) ) ;
#6823=EDGE_LOOP ( 'NONE', ( #1447, #6174, #7116 ) ) ;
#6834=AXIS2_PLACEMENT_3D ( 'NONE', #17, #6720, #1465 ) ;
#6836=EDGE_CURVE ( 'NONE', #951, #2228, #7, .T. ) ;
#6840=CARTESIAN_POINT ( 'NONE',  ( 0.3403864257300893703, -0.2263128404110642256, 0.1985658431051765538 ) ) ;
#6849=CARTESIAN_POINT ( 'NONE',  ( 0.3442723180357227797, 0.1814473180894613513, -0.2762752072743030474 ) ) ;
#6854=CARTESIAN_POINT ( 'NONE',  ( 0.3485777078273625817, 0.2029921329169074307, 0.2518088348849962799 ) ) ;
#6858=VERTEX_POINT ( 'NONE', #765 ) ;
#6876=DIRECTION ( 'NONE',  ( -0.000000000000000000, 1.000000000000000000, 1.224646799147353207E-16 ) ) ;
#6881=ORIENTED_EDGE ( 'NONE', *, *, #3657, .T. ) ;
#6884=ORIENTED_EDGE ( 'NONE', *, *, #376, .T. ) ;
#6902=PLANE ( 'NONE',  #5922 ) ;
#6933=B_SPLINE_CURVE_WITH_KNOTS ( 'NONE', 3,
 ( #3767, #6104, #5571, #254, #859, #6787 ),
 .UNSPECIFIED., .F., .F.,
 ( 4, 2, 4 ),
 ( 0.000000000000000000, 0.0001677595217559108194, 0.0003355190435118216388 ),
 .UNSPECIFIED. ) ;
#6935=CARTESIAN_POINT ( 'NONE',  ( 0.3581828924050324825, 0.3486337532542225226, 1.056976728655274672E-17 ) ) ;
#6940=CARTESIAN_POINT ( 'NONE',  ( 0.3483227611829849413, -0.3409548833797009237, 0.000000000000000000 ) ) ;
#6959=EDGE_LOOP ( 'NONE', ( #6280, #363, #6884 ) ) ;
#6980=CARTESIAN_POINT ( 'NONE',  ( 0.3581828924050327045, -0.3486337532542230222, -1.123169198254405176E-18 ) ) ;
#6988=CARTESIAN_POINT ( 'NONE',  ( 0.3574299024618896592, -0.1732824651941382854, 0.3001340337771306044 ) ) ;
#7019=CARTESIAN_POINT ( 'NONE',  ( 0.3585569304025113535, 0.1763492631043844516, -0.3019338371022697864 ) ) ;
#7029=EDGE_LOOP ( 'NONE', ( #3015, #1415, #1615 ) ) ;
#7035=DIRECTION ( 'NONE',  ( 0.000000000000000000, 0.000000000000000000, -1.000000000000000000 ) ) ;
#7042=ORIENTED_EDGE ( 'NONE', *, *, #1290, .F. ) ;
#7084=CARTESIAN_POINT ( 'NONE',  ( 0.3487098613656773316, 0.1177053732609037312, 0.3017042368166658051 ) ) ;
#7089=ORIENTED_EDGE ( 'NONE', *, *, #2275, .F. ) ;
#7091=EDGE_CURVE ( 'NONE', #3441, #3901, #7396, .T. ) ;
#7092=FACE_OUTER_BOUND ( 'NONE', #4935, .T. ) ;
#7095=CARTESIAN_POINT ( 'NONE',  ( 0.3322355029819564209, 0.06185644463604170890, -0.2952755905511810774 ) ) ;
#7112=VERTEX_POINT ( 'NONE', #3753 ) ;
#7115=AXIS2_PLACEMENT_3D ( 'NONE', #4077, #1770, #2277 ) ;
#7116=ORIENTED_EDGE ( 'NONE', *, *, #6645, .F. ) ;
#7125=CARTESIAN_POINT ( 'NONE',  ( 0.3426140154788509529, 0.05854580700589206294, 0.3015405874046677703 ) ) ;
#7133=CARTESIAN_POINT ( 'NONE',  ( 0.3528822938286762523, 0.1453909600788098055, -0.3018098512751524187 ) ) ;
#7134=ADVANCED_FACE ( 'NONE', ( #6091 ), #3552, .T. ) ;
#7135=CARTESIAN_POINT ( 'NONE',  ( 0.02637295201093722841, 0.3409548833797004797, 3.882420715168025960E-18 ) ) ;
#7137=CARTESIAN_POINT ( 'NONE',  ( 0.3306743754077736130, -0.2557161625347756373, -0.1476377952755904555 ) ) ;
#7156=CARTESIAN_POINT ( 'NONE',  ( 0.3496875272944831026, -0.3447318307381757041, 0.006541864722391225496 ) ) ;
#7159=CARTESIAN_POINT ( 'NONE',  ( 0.3321019207957557895, 0.02907045490630093265, 0.2952755905511811330 ) ) ;
#7162=CARTESIAN_POINT ( 'NONE',  ( 0.3496779274129791504, 0.1667266398149495066, 0.3017721699676332303 ) ) ;
#7164=EDGE_LOOP ( 'NONE', ( #4941, #236, #4060, #2755 ) ) ;
#7169=CARTESIAN_POINT ( 'NONE',  ( 0.4685039370078740717, 0.000000000000000000, 0.000000000000000000 ) ) ;
#7171=AXIS2_PLACEMENT_3D ( 'NONE', #3720, #1406, #5597 ) ;
#7172=CARTESIAN_POINT ( 'NONE',  ( 0.3528850351813196951, 0.1886720902358826890, -0.2768301761068310274 ) ) ;
#7181=B_SPLINE_CURVE_WITH_KNOTS ( 'NONE', 3,
 ( #5557, #804, #2108, #384, #4936, #4439 ),
 .UNSPECIFIED., .F., .F.,
 ( 4, 2, 4 ),
 ( 2.380732026380572752E-07, 0.002190927868076664002, 0.004381617662950689981 ),
 .UNSPECIFIED. ) ;
#7189=CARTESIAN_POINT ( 'NONE',  ( 0.3565422270302660013, -0.3441025489056189213, 0.005451916616122784963 ) ) ;
#7192=CARTESIAN_POINT ( 'NONE',  ( 0.01834252172841640063, -0.1843865549457986697, 0.2711842997036482683 ) ) ;
#7205=DIRECTION ( 'NONE',  ( 1.000000000000000000, 0.000000000000000000, 0.000000000000000000 ) ) ;
#7206=AXIS2_PLACEMENT_3D ( 'NONE', #295, #2503, #2614 ) ;
#7216=CARTESIAN_POINT ( 'NONE',  ( 0.3391892065151631552, -0.3125419764313924209, 0.04921259842519686012 ) ) ;
#7220=CARTESIAN_POINT ( 'NONE',  ( 0.3581828924050323715, 0.1743168766271107895, -0.3019256869348722061 ) ) ;
#7222=VECTOR ( 'NONE', #3635, 39.37007874015748143 ) ;
#7243=EDGE_CURVE ( 'NONE', #1005, #913, #14, .T. ) ;
#7246=FACE_OUTER_BOUND ( 'NONE', #486, .T. ) ;
#7260=CARTESIAN_POINT ( 'NONE',  ( 0.000000000000000000, 0.000000000000000000, -0.2952755905511810774 ) ) ;
#7269=ORIENTED_EDGE ( 'NONE', *, *, #83, .F. ) ;
#7282=CARTESIAN_POINT ( 'NONE',  ( 0.3574269917172684941, -0.1732784665916271005, -0.3001271079943088615 ) ) ;
#7289=B_SPLINE_CURVE_WITH_KNOTS ( 'NONE', 3,
 ( #994, #3211, #7512, #5812, #1635, #3399 ),
 .UNSPECIFIED., .F., .F.,
 ( 4, 2, 4 ),
 ( 2.380732026382070147E-07, 0.002190927868076674410, 0.004381617662950710798 ),
 .UNSPECIFIED. ) ;
#7298=ORIENTED_EDGE ( 'NONE', *, *, #6836, .F. ) ;
#7311=ORIENTED_EDGE ( 'NONE', *, *, #1639, .F. ) ;
#7314=CARTESIAN_POINT ( 'NONE',  ( 0.000000000000000000, -0.2557161625347748601, 0.1476377952755911216 ) ) ;
#7328=CARTESIAN_POINT ( 'NONE',  ( 0.3483227611829846082, 0.1704774416898497680, -0.2952755905511810774 ) ) ;
#7341=CARTESIAN_POINT ( 'NONE',  ( 0.000000000000000000, -0.2557161625347750822, -0.1476377952755907330 ) ) ;
#7342=CARTESIAN_POINT ( 'NONE',  ( 0.3426404862726870615, 0.2318193597401792261, 0.2015595396344879719 ) ) ;
#7356=CARTESIAN_POINT ( 'NONE',  ( 0.000000000000000000, 0.000000000000000000, 0.000000000000000000 ) ) ;
#7363=ORIENTED_EDGE ( 'NONE', *, *, #2754, .F. ) ;
#7367=CARTESIAN_POINT ( 'NONE',  ( 0.3527006543068523237, 0.1709223289430787940, -0.2960461578774135072 ) ) ;
#7373=CARTESIAN_POINT ( 'NONE',  ( 0.3565422270302655572, 0.1673297761639317704, -0.3007275071673040645 ) ) ;
#7380=CARTESIAN_POINT ( 'NONE',  ( 0.3528850351813199171, 0.3340780101605773655, 0.02497973507596915402 ) ) ;
#7389=EDGE_CURVE ( 'NONE', #698, #2401, #4954, .T. ) ;
#7390=CARTESIAN_POINT ( 'NONE',  ( 0.3398312250857989381, 0.3151631602416481437, 0.04467257488985636182 ) ) ;
#7391=EDGE_LOOP ( 'NONE', ( #5333, #1185, #4378 ) ) ;
#7392=CARTESIAN_POINT ( 'NONE',  ( 0.000000000000000000, 2.892866454678787531E-17, -0.2362204724409449064 ) ) ;
#7396=B_SPLINE_CURVE_WITH_KNOTS ( 'NONE', 3,
 ( #7260, #6661, #3828, #2033, #1515, #4361 ),
 .UNSPECIFIED., .F., .F.,
 ( 4, 2, 4 ),
 ( 0.02625214965902978106, 0.02844383079405753134, 0.03063551192908527815 ),
 .UNSPECIFIED. ) ;
#7399=EDGE_LOOP ( 'NONE', ( #3177, #1619 ) ) ;
#7400=CARTESIAN_POINT ( 'NONE',  ( 0.002513486811083624848, -0.2845799557467911245, 0.09764423893321799719 ) ) ;
#7401=CARTESIAN_POINT ( 'NONE',  ( 0.3459463601587710602, -0.3157502742997210787, 0.04365566351110977683 ) ) ;
#7411=CARTESIAN_POINT ( 'NONE',  ( 1.055789886223273654E-16, -0.2411939993270979798, -0.1727909197870958757 ) ) ;
#7420=VERTEX_POINT ( 'NONE', #3237 ) ;
#7424=CARTESIAN_POINT ( 'NONE',  ( 0.3322361761492683696, 0.2247851515112334331, 0.2012118778978378431 ) ) ;
#7431=CARTESIAN_POINT ( 'NONE',  ( 3.027559055118110187, 0.000000000000000000, 0.000000000000000000 ) ) ;
#7438=CARTESIAN_POINT ( 'NONE',  ( 0.3585569128062321420, -0.3496569568119795024, -0.001755940978325754281 ) ) ;
#7440=CARTESIAN_POINT ( 'NONE',  ( 0.3410249605999410294, -1.062517223525361548E-12, -0.3014927230551905368 ) ) ;
#7452=ORIENTED_EDGE ( 'NONE', *, *, #1154, .T. ) ;
#7467=FACE_OUTER_BOUND ( 'NONE', #4659, .T. ) ;
#7478=CARTESIAN_POINT ( 'NONE',  ( 3.027559055118110187, 0.000000000000000000, 0.1982677165354330695 ) ) ;
#7480=CONICAL_SURFACE ( 'NONE', #1472, 0.2952755905511810774, 1.047197551196600518 ) ;
#7488=VERTEX_POINT ( 'NONE', #3816 ) ;
#7492=CARTESIAN_POINT ( 'NONE',  ( 0.3483227611829848303, -0.1704774416898505729, -0.2952755905511810774 ) ) ;
#7495=CARTESIAN_POINT ( 'NONE',  ( 0.3410249605999410294, 1.062103031354818709E-12, 0.3014927230551906479 ) ) ;
#7501=CARTESIAN_POINT ( 'NONE',  ( 0.3527006543068526567, -0.3418446578861590868, 8.418741006566202135E-18 ) ) ;
#7506=CARTESIAN_POINT ( 'NONE',  ( 0.3410425348215777031, -0.2462961272004795532, -0.1763890642357578975 ) ) ;
#7512=CARTESIAN_POINT ( 'NONE',  ( 0.01168997831664865018, 0.3129651733100085598, -0.04847959992982851796 ) ) ;
#7514=EDGE_CURVE ( 'NONE', #5565, #5211, #2226, .T. ) ;
#7581=COLOUR_RGB('Black',0.12,0.14,0.17);
#7582=FILL_AREA_STYLE_COLOUR('',#7581);
#7583=FILL_AREA_STYLE('',(#7582));
#7584=SURFACE_STYLE_FILL_AREA(#7583);
#7585=SURFACE_SIDE_STYLE('',(#7584));
#7586=SURFACE_STYLE_USAGE(.BOTH.,#7585);
#7587=PRESENTATION_STYLE_ASSIGNMENT((#7586));
ENDSEC;
END-ISO-10303-21;
